ISO-10303-21;
HEADER;
FILE_DESCRIPTION (('STEP AP203'),
    '1' );
FILE_NAME ('Locking Button_Varsayılan.step',
    '2026-10-08T23:54:15',
    ( '' ),
    ( '' ),
    'SwSTEP 2.0',
    'SolidWorks 2024',
    '' );
FILE_SCHEMA (( 'AUTOMOTIVE_DESIGN' ));
ENDSEC;

DATA;
#87=CARTESIAN_POINT ( 'NONE',  ( -8.160000000000000142, -9.652339641703484574, -1.621096496867199033 ) ) ;
#114=EDGE_LOOP ( 'NONE', ( #28040, #100187, #84080, #84178 ) ) ;
#174=EDGE_LOOP ( 'NONE', ( #58420, #72344, #98648 ) ) ;
#188=ADVANCED_FACE ( 'NONE', ( #94676 ), #86066, .T. ) ;
#253=ORIENTED_EDGE ( 'NONE', *, *, #52923, .F. ) ;
#290=EDGE_CURVE ( 'NONE', #36098, #73116, #17648, .T. ) ;
#307=ORIENTED_EDGE ( 'NONE', *, *, #64377, .T. ) ;
#586=CARTESIAN_POINT ( 'NONE',  ( 8.160000000000000142, -2.191226316053958875E-18, 2.701633758479787833E-17 ) ) ;
#599=DIRECTION ( 'NONE',  ( 0.000000000000000000, 0.000000000000000000, -1.000000000000000000 ) ) ;
#725=ORIENTED_EDGE ( 'NONE', *, *, #42551, .T. ) ;
#759=EDGE_CURVE ( 'NONE', #82155, #14495, #100103, .T. ) ;
#766=B_SPLINE_CURVE_WITH_KNOTS ( 'NONE', 3,
 ( #71091, #41147, #3090, #48763, #55877, #78669 ),
 .UNSPECIFIED., .F., .F.,
 ( 4, 2, 4 ),
 ( 0.0004434240296263077972, 0.001023314793611319017, 0.001603205557596327959 ),
 .UNSPECIFIED. ) ;
#775=CARTESIAN_POINT ( 'NONE',  ( 8.160000000000000142, 9.789768006247301813, -0.8564937190954607926 ) ) ;
#791=CYLINDRICAL_SURFACE ( 'NONE', #74774, 1.699999999999999734 ) ;
#808=ORIENTED_EDGE ( 'NONE', *, *, #72055, .T. ) ;
#812=DIRECTION ( 'NONE',  ( 0.000000000000000000, 0.000000000000000000, -1.000000000000000000 ) ) ;
#856=ADVANCED_FACE ( 'NONE', ( #96063 ), #49405, .F. ) ;
#891=CARTESIAN_POINT ( 'NONE',  ( 6.660000000000001030, -10.15233964170348457, -1.303165529866009420 ) ) ;
#936=CARTESIAN_POINT ( 'NONE',  ( -8.094297649259210914, -10.08546205824535669, 1.310587897985993955 ) ) ;
#1068=DIRECTION ( 'NONE',  ( 0.000000000000000000, 0.000000000000000000, -1.000000000000000000 ) ) ;
#1091=EDGE_LOOP ( 'NONE', ( #49889, #307, #15501, #45982, #27971, #95161, #30577, #51579 ) ) ;
#1118=CIRCLE ( 'NONE', #27053, 1.306876713926001354 ) ;
#1159=ADVANCED_FACE ( 'NONE', ( #70104 ), #60998, .T. ) ;
#1241=EDGE_CURVE ( 'NONE', #19777, #34658, #46760, .T. ) ;
#1305=AXIS2_PLACEMENT_3D ( 'NONE', #64858, #9533, #88669 ) ;
#1308=EDGE_LOOP ( 'NONE', ( #60717, #42717, #64099, #6541, #66658 ) ) ;
#1313=ORIENTED_EDGE ( 'NONE', *, *, #36693, .T. ) ;
#1344=AXIS2_PLACEMENT_3D ( 'NONE', #12698, #49296, #4109 ) ;
#1366=( LENGTH_UNIT ( ) NAMED_UNIT ( * ) SI_UNIT ( .MILLI., .METRE. ) );
#1373=CARTESIAN_POINT ( 'NONE',  ( 8.160000000000000142, -9.652339641703484574, 1.628518864987183790 ) ) ;
#1405=DIRECTION ( 'NONE',  ( 0.000000000000000000, -0.000000000000000000, -1.000000000000000000 ) ) ;
#1468=CARTESIAN_POINT ( 'NONE',  ( 8.160000000000000142, -10.15233964170348457, 0.003711184059992174607 ) ) ;
#1479=ORIENTED_EDGE ( 'NONE', *, *, #26398, .F. ) ;
#1499=VERTEX_POINT ( 'NONE', #44658 ) ;
#1505=CARTESIAN_POINT ( 'NONE',  ( -8.160000000000000142, -10.65233964170348635, -1.621096496867198589 ) ) ;
#1533=CARTESIAN_POINT ( 'NONE',  ( 0.000000000000000000, 0.000000000000000000, 0.000000000000000000 ) ) ;
#1559=CARTESIAN_POINT ( 'NONE',  ( 7.160000000000000142, -9.123836073446797812, -2.666350264951732552 ) ) ;
#1621=AXIS2_PLACEMENT_3D ( 'NONE', #78289, #62588, #52980 ) ;
#1639=DIRECTION ( 'NONE',  ( -1.000000000000000000, -0.000000000000000000, -0.000000000000000000 ) ) ;
#1686=CIRCLE ( 'NONE', #87586, 2.399999999999999911 ) ;
#1769=CARTESIAN_POINT ( 'NONE',  ( -11.16000000000000014, -10.65233964170348635, -1.621096496867199033 ) ) ;
#1815=CARTESIAN_POINT ( 'NONE',  ( -8.160000000000000142, -10.15233964170348457, 1.310587897985993955 ) ) ;
#1827=AXIS2_PLACEMENT_3D ( 'NONE', #19543, #97175, #40888 ) ;
#1833=CARTESIAN_POINT ( 'NONE',  ( -6.660000000000001030, 0.000000000000000000, 0.000000000000000000 ) ) ;
#1861=DIRECTION ( 'NONE',  ( 1.000000000000000000, 0.000000000000000000, 0.000000000000000000 ) ) ;
#1917=CARTESIAN_POINT ( 'NONE',  ( 16.36243866176394945, 0.000000000000000000, 2.399999999999999911 ) ) ;
#2005=DIRECTION ( 'NONE',  ( 0.000000000000000000, 0.9513357669802769978, -0.3081562241202474572 ) ) ;
#2022=EDGE_CURVE ( 'NONE', #46703, #34658, #11339, .T. ) ;
#2051=EDGE_CURVE ( 'NONE', #38938, #45450, #65158, .T. ) ;
#2113=LINE ( 'NONE', #33048, #79722 ) ;
#2130=DIRECTION ( 'NONE',  ( 0.000000000000000000, 0.3081562241202472907, 0.9513357669802769978 ) ) ;
#2235=AXIS2_PLACEMENT_3D ( 'NONE', #66799, #67286, #21087 ) ;
#2259=DIRECTION ( 'NONE',  ( 0.000000000000000000, 0.000000000000000000, 1.000000000000000000 ) ) ;
#2306=ORIENTED_EDGE ( 'NONE', *, *, #10597, .T. ) ;
#2483=CARTESIAN_POINT ( 'NONE',  ( 8.160000000000000142, -10.65233964170348635, 1.211157557776864291 ) ) ;
#2551=ORIENTED_EDGE ( 'NONE', *, *, #96329, .T. ) ;
#2592=CARTESIAN_POINT ( 'NONE',  ( -8.160000000000000142, -9.652339641703484574, -1.203735189656879756 ) ) ;
#2663=DIRECTION ( 'NONE',  ( -7.719682517540865740E-16, -0.4450093991605197363, 0.8955258983741304357 ) ) ;
#2685=VECTOR ( 'NONE', #61208, 1000.000000000000114 ) ;
#2715=CARTESIAN_POINT ( 'NONE',  ( -7.160000000000000142, -10.77121780415746599, 1.154761385154455366 ) ) ;
#2726=AXIS2_PLACEMENT_3D ( 'NONE', #91133, #66831, #75400 ) ;
#2760=DIRECTION ( 'NONE',  ( -1.000000000000000000, 0.000000000000000000, 0.000000000000000000 ) ) ;
#2788=CARTESIAN_POINT ( 'NONE',  ( -6.660000000000001030, -11.08332949055823846, -0.7794760011071779626 ) ) ;
#2896=EDGE_CURVE ( 'NONE', #60171, #62319, #6300, .T. ) ;
#2947=DIRECTION ( 'NONE',  ( 0.000000000000000000, 0.000000000000000000, 1.000000000000000000 ) ) ;
#2983=ORIENTED_EDGE ( 'NONE', *, *, #54716, .T. ) ;
#3009=EDGE_CURVE ( 'NONE', #43349, #54056, #22502, .T. ) ;
#3020=VERTEX_POINT ( 'NONE', #67392 ) ;
#3090=CARTESIAN_POINT ( 'NONE',  ( 7.853763894818856173, -10.48276843398940272, 1.273485471867758401 ) ) ;
#3148=ORIENTED_EDGE ( 'NONE', *, *, #56843, .T. ) ;
#3260=ORIENTED_EDGE ( 'NONE', *, *, #73861, .T. ) ;
#3424=TOROIDAL_SURFACE ( 'NONE', #21267, 19.00000000000000355, 1.000000000000000000 ) ;
#3444=PLANE ( 'NONE',  #1305 ) ;
#3548=ORIENTED_EDGE ( 'NONE', *, *, #28502, .F. ) ;
#3612=DIRECTION ( 'NONE',  ( 1.000000000000000000, 0.000000000000000000, 0.000000000000000000 ) ) ;
#3657=DIRECTION ( 'NONE',  ( 0.000000000000000000, 0.000000000000000000, -1.000000000000000000 ) ) ;
#3739=CARTESIAN_POINT ( 'NONE',  ( 1.542438661763949392, 0.000000000000000000, 2.399999999999999911 ) ) ;
#3781=EDGE_CURVE ( 'NONE', #97633, #29959, #97302, .T. ) ;
#3797=VERTEX_POINT ( 'NONE', #22689 ) ;
#3824=EDGE_LOOP ( 'NONE', ( #19718, #49691, #50337, #64827, #54737, #69528, #42189, #8083, #70023, #34708, #66887, #32644 ) ) ;
#3875=LINE ( 'NONE', #5355, #49611 ) ;
#3924=ORIENTED_EDGE ( 'NONE', *, *, #71796, .T. ) ;
#3927=DIRECTION ( 'NONE',  ( 1.000000000000000000, 0.000000000000000000, 0.000000000000000000 ) ) ;
#3928=CARTESIAN_POINT ( 'NONE',  ( 11.16000000000000014, -10.65233964170348635, -1.621096496867198589 ) ) ;
#4109=DIRECTION ( 'NONE',  ( 0.000000000000000000, 0.000000000000000000, -1.000000000000000000 ) ) ;
#4137=ORIENTED_EDGE ( 'NONE', *, *, #99840, .T. ) ;
#4151=CARTESIAN_POINT ( 'NONE',  ( -6.660000000000001030, 0.000000000000000000, 0.000000000000000000 ) ) ;
#4158=DIRECTION ( 'NONE',  ( -1.000000000000000000, -0.000000000000000000, -0.000000000000000000 ) ) ;
#4241=CIRCLE ( 'NONE', #60965, 1.306876713926001354 ) ;
#4305=VECTOR ( 'NONE', #46008, 1000.000000000000000 ) ;
#4487=APPLICATION_CONTEXT ( 'configuration controlled 3d designs of mechanical parts and assemblies' ) ;
#4552=FACE_OUTER_BOUND ( 'NONE', #85461, .T. ) ;
#4670=FACE_OUTER_BOUND ( 'NONE', #34109, .T. ) ;
#4760=LINE ( 'NONE', #66687, #16211 ) ;
#4780=VERTEX_POINT ( 'NONE', #33960 ) ;
#4811=ORIENTED_EDGE ( 'NONE', *, *, #60333, .F. ) ;
#4814=ORIENTED_EDGE ( 'NONE', *, *, #40684, .F. ) ;
#4831=FACE_OUTER_BOUND ( 'NONE', #28425, .T. ) ;
#4948=VECTOR ( 'NONE', #26791, 1000.000000000000000 ) ;
#4952=CARTESIAN_POINT ( 'NONE',  ( -8.160000000000000142, -9.652339641703484574, 1.628518864987183790 ) ) ;
#4953=CARTESIAN_POINT ( 'NONE',  ( -6.660000000000001030, -9.572916487583201572, -0.7764348688322061376 ) ) ;
#5112=CARTESIAN_POINT ( 'NONE',  ( -11.16000000000000014, -10.15233964170348457, 0.003711184059992174607 ) ) ;
#5143=EDGE_CURVE ( 'NONE', #82230, #13329, #10376, .T. ) ;
#5183=CARTESIAN_POINT ( 'NONE',  ( 8.160000000000000142, 2.939152317953647106E-16, -2.399999999999999911 ) ) ;
#5196=EDGE_CURVE ( 'NONE', #51347, #80380, #25378, .T. ) ;
#5227=ORIENTED_EDGE ( 'NONE', *, *, #9170, .T. ) ;
#5249=EDGE_LOOP ( 'NONE', ( #34872, #41207, #93473, #65946 ) ) ;
#5299=LINE ( 'NONE', #58595, #21444 ) ;
#5307=CARTESIAN_POINT ( 'NONE',  ( 11.16000000000000014, -10.15233964170348457, 0.003711184059992174607 ) ) ;
#5314=SPHERICAL_SURFACE ( 'NONE', #47992, 1.000000000000000000 ) ;
#5319=VECTOR ( 'NONE', #8927, 1000.000000000000000 ) ;
#5321=CARTESIAN_POINT ( 'NONE',  ( -11.16000000000000014, -10.15233964170348457, 0.003711184059992174607 ) ) ;
#5332=VECTOR ( 'NONE', #17495, 1000.000000000000000 ) ;
#5337=ADVANCED_FACE ( 'NONE', ( #31212 ), #23588, .T. ) ;
#5346=EDGE_CURVE ( 'NONE', #22875, #29959, #9375, .T. ) ;
#5350=VERTEX_POINT ( 'NONE', #96124 ) ;
#5355=CARTESIAN_POINT ( 'NONE',  ( 8.160000000000000142, 10.80195425911416507, -0.9450485415980990345 ) ) ;
#5395=ORIENTED_EDGE ( 'NONE', *, *, #3781, .T. ) ;
#5421=ORIENTED_EDGE ( 'NONE', *, *, #22805, .F. ) ;
#5422=DIRECTION ( 'NONE',  ( 0.000000000000000000, -0.9961946980917452121, 0.08715574274766166307 ) ) ;
#5478=CIRCLE ( 'NONE', #2235, 2.399999999999999911 ) ;
#5567=EDGE_CURVE ( 'NONE', #70921, #53265, #83877, .T. ) ;
#5648=EDGE_CURVE ( 'NONE', #99058, #75155, #98300, .T. ) ;
#5672=AXIS2_PLACEMENT_3D ( 'NONE', #87597, #47539, #1861 ) ;
#5769=CARTESIAN_POINT ( 'NONE',  ( 8.160000000000000142, 0.000000000000000000, 2.399999999999999911 ) ) ;
#5872=VERTEX_POINT ( 'NONE', #96493 ) ;
#5885=ORIENTED_EDGE ( 'NONE', *, *, #9249, .T. ) ;
#5910=FACE_OUTER_BOUND ( 'NONE', #1091, .T. ) ;
#6047=FACE_BOUND ( 'NONE', #63065, .T. ) ;
#6072=DIRECTION ( 'NONE',  ( 0.000000000000000000, 1.000000000000000000, 0.000000000000000000 ) ) ;
#6080=CARTESIAN_POINT ( 'NONE',  ( -8.160000000000000142, -9.728493947732140157, 1.239948043688426926 ) ) ;
#6173=CARTESIAN_POINT ( 'NONE',  ( 6.660000000000001030, 1.527978830621527617, 4.717155776778118259 ) ) ;
#6241=ORIENTED_EDGE ( 'NONE', *, *, #24909, .T. ) ;
#6249=ADVANCED_FACE ( 'NONE', ( #52087 ), #44477, .F. ) ;
#6300=CIRCLE ( 'NONE', #63030, 1.000000000000000222 ) ;
#6313=ORIENTED_EDGE ( 'NONE', *, *, #85647, .T. ) ;
#6328=DIRECTION ( 'NONE',  ( -1.000000000000000000, -0.000000000000000000, -0.000000000000000000 ) ) ;
#6376=VECTOR ( 'NONE', #29885, 999.9999999999998863 ) ;
#6423=DIRECTION ( 'NONE',  ( 0.000000000000000000, 0.000000000000000000, -1.000000000000000000 ) ) ;
#6439=CARTESIAN_POINT ( 'NONE',  ( 7.160000000000000142, -0.1502355682624769706, 6.837492552117866218 ) ) ;
#6451=LINE ( 'NONE', #29284, #99557 ) ;
#6485=EDGE_CURVE ( 'NONE', #31685, #57944, #41356, .T. ) ;
#6530=ORIENTED_EDGE ( 'NONE', *, *, #61002, .T. ) ;
#6541=ORIENTED_EDGE ( 'NONE', *, *, #26398, .T. ) ;
#6551=CARTESIAN_POINT ( 'NONE',  ( -6.660000000000001030, 0.000000000000000000, 0.000000000000000000 ) ) ;
#6582=CARTESIAN_POINT ( 'NONE',  ( -7.160000000000000142, -0.1502355682624769706, 6.837492552117866218 ) ) ;
#6583=ORIENTED_EDGE ( 'NONE', *, *, #55227, .F. ) ;
#6782=VECTOR ( 'NONE', #43663, 1000.000000000000114 ) ;
#6787=ADVANCED_FACE ( 'NONE', ( #86898 ), #47346, .F. ) ;
#6794=ORIENTED_EDGE ( 'NONE', *, *, #7716, .F. ) ;
#6895=CARTESIAN_POINT ( 'NONE',  ( 7.666860990600891768, 10.67251638830246918, -0.9337241952711420323 ) ) ;
#6966=FACE_OUTER_BOUND ( 'NONE', #8138, .T. ) ;
#7036=DIRECTION ( 'NONE',  ( 1.000000000000000000, -0.000000000000000000, 0.000000000000000000 ) ) ;
#7043=ADVANCED_FACE ( 'NONE', ( #86283 ), #70559, .F. ) ;
#7046=ORIENTED_EDGE ( 'NONE', *, *, #85647, .F. ) ;
#7055=DIRECTION ( 'NONE',  ( -0.000000000000000000, -0.9513357669802769978, 0.3081562241202474572 ) ) ;
#7111=DIRECTION ( 'NONE',  ( 1.000000000000000000, -0.000000000000000000, 0.000000000000000000 ) ) ;
#7136=EDGE_LOOP ( 'NONE', ( #20316, #63931, #70856, #50141 ) ) ;
#7188=CYLINDRICAL_SURFACE ( 'NONE', #70183, 1.699999999999999289 ) ;
#7219=VECTOR ( 'NONE', #13913, 1000.000000000000000 ) ;
#7226=ORIENTED_EDGE ( 'NONE', *, *, #43174, .T. ) ;
#7384=VERTEX_POINT ( 'NONE', #67938 ) ;
#7385=CARTESIAN_POINT ( 'NONE',  ( 8.035386273831683468, 10.29654910626257802, -0.9008313202359966576 ) ) ;
#7408=DIRECTION ( 'NONE',  ( -1.000000000000000000, -0.000000000000000000, -0.000000000000000000 ) ) ;
#7470=FACE_OUTER_BOUND ( 'NONE', #77145, .T. ) ;
#7495=EDGE_CURVE ( 'NONE', #5872, #64045, #77084, .T. ) ;
#7499=LINE ( 'NONE', #61805, #31870 ) ;
#7562=LINE ( 'NONE', #100384, #14194 ) ;
#7665=CARTESIAN_POINT ( 'NONE',  ( 8.160000000000000142, -10.65233964170348635, -1.621096496867198589 ) ) ;
#7688=ORIENTED_EDGE ( 'NONE', *, *, #53630, .T. ) ;
#7704=DIRECTION ( 'NONE',  ( -1.000000000000000000, 0.000000000000000000, 0.000000000000000000 ) ) ;
#7716=EDGE_CURVE ( 'NONE', #18728, #55102, #18075, .T. ) ;
#7802=DIRECTION ( 'NONE',  ( 1.000000000000000000, -0.000000000000000000, 0.000000000000000000 ) ) ;
#7825=AXIS2_PLACEMENT_3D ( 'NONE', #87, #39142, #99029 ) ;
#7845=CARTESIAN_POINT ( 'NONE',  ( -8.160000000000000142, -10.15233964170348457, 0.003711184059992174607 ) ) ;
#7890=LINE ( 'NONE', #99722, #2685 ) ;
#7891=CARTESIAN_POINT ( 'NONE',  ( 11.16000000000000014, -10.15233964170348457, 0.003711184059992174607 ) ) ;
#7909=ADVANCED_FACE ( 'NONE', ( #68811 ), #31743, .T. ) ;
#7963=ADVANCED_FACE ( 'NONE', ( #45486 ), #791, .T. ) ;
#7977=DIRECTION ( 'NONE',  ( 1.000000000000000000, 0.000000000000000000, 0.000000000000000000 ) ) ;
#8000=DIRECTION ( 'NONE',  ( 0.000000000000000000, -0.9967269304714136968, -0.08084198211964954695 ) ) ;
#8027=AXIS2_PLACEMENT_3D ( 'NONE', #42198, #18824, #95957 ) ;
#8083=ORIENTED_EDGE ( 'NONE', *, *, #30278, .F. ) ;
#8109=ORIENTED_EDGE ( 'NONE', *, *, #52984, .F. ) ;
#8138=EDGE_LOOP ( 'NONE', ( #64333, #91377, #20112, #10890, #74499, #98495, #44932, #12136, #87011 ) ) ;
#8282=ORIENTED_EDGE ( 'NONE', *, *, #66637, .T. ) ;
#8332=MANIFOLD_SOLID_BREP ( 'Radyus2', #12780 ) ;
#8444=DIRECTION ( 'NONE',  ( 0.000000000000000000, 0.000000000000000000, -1.000000000000000000 ) ) ;
#8452=SPHERICAL_SURFACE ( 'NONE', #56099, 1.000000000000000000 ) ;
#8699=AXIS2_PLACEMENT_3D ( 'NONE', #34550, #11207, #73118 ) ;
#8714=CARTESIAN_POINT ( 'NONE',  ( -11.16000000000000014, -10.65233964170348635, -1.621096496867198589 ) ) ;
#8775=CARTESIAN_POINT ( 'NONE',  ( 8.160000000000000142, -9.652339641703484574, -1.203735189656879756 ) ) ;
#8904=DIRECTION ( 'NONE',  ( 0.000000000000000000, 0.000000000000000000, 1.000000000000000000 ) ) ;
#8927=DIRECTION ( 'NONE',  ( 1.000000000000000000, -0.000000000000000000, -0.000000000000000000 ) ) ;
#9120=ORIENTED_EDGE ( 'NONE', *, *, #20552, .F. ) ;
#9170=EDGE_CURVE ( 'NONE', #51347, #45568, #91644, .T. ) ;
#9215=AXIS2_PLACEMENT_3D ( 'NONE', #33862, #10020, #3927 ) ;
#9238=CARTESIAN_POINT ( 'NONE',  ( -8.160000000000000142, -9.652339641703484574, -1.621096496867199033 ) ) ;
#9249=EDGE_CURVE ( 'NONE', #20729, #87025, #19800, .T. ) ;
#9367=EDGE_CURVE ( 'NONE', #82473, #46259, #15019, .T. ) ;
#9375=LINE ( 'NONE', #40334, #28557 ) ;
#9533=DIRECTION ( 'NONE',  ( 0.000000000000000000, 0.08084198211964954695, -0.9967269304714136968 ) ) ;
#9592=DIRECTION ( 'NONE',  ( 0.000000000000000000, 0.000000000000000000, -1.000000000000000000 ) ) ;
#9647=ORIENTED_EDGE ( 'NONE', *, *, #759, .F. ) ;
#9648=AXIS2_PLACEMENT_3D ( 'NONE', #5112, #97944, #36062 ) ;
#9686=CARTESIAN_POINT ( 'NONE',  ( 6.660000000000001030, -2.191226316053958875E-18, 2.701633758479787833E-17 ) ) ;
#9692=DIRECTION ( 'NONE',  ( 1.000000000000000000, 0.000000000000000000, 0.000000000000000000 ) ) ;
#9724=CIRCLE ( 'NONE', #66474, 2.899999999999999911 ) ;
#9759=FACE_OUTER_BOUND ( 'NONE', #54566, .T. ) ;
#9811=EDGE_CURVE ( 'NONE', #11540, #68689, #5299, .T. ) ;
#9828=ORIENTED_EDGE ( 'NONE', *, *, #64449, .T. ) ;
#9891=DIRECTION ( 'NONE',  ( 0.000000000000000000, -0.9967269304714136968, -0.08084198211964954695 ) ) ;
#9945=CARTESIAN_POINT ( 'NONE',  ( 6.660000000000001030, -0.2368809837866516499, 5.288828319098142217 ) ) ;
#9953=ADVANCED_FACE ( 'NONE', ( #82796 ), #44749, .T. ) ;
#10014=EDGE_CURVE ( 'NONE', #61766, #32857, #34448, .T. ) ;
#10017=ORIENTED_EDGE ( 'NONE', *, *, #99155, .T. ) ;
#10020=DIRECTION ( 'NONE',  ( 0.000000000000000000, 1.000000000000000000, 0.000000000000000000 ) ) ;
#10077=EDGE_CURVE ( 'NONE', #31685, #20729, #21879, .T. ) ;
#10146=CIRCLE ( 'NONE', #23084, 19.00000000000000000 ) ;
#10188=DIRECTION ( 'NONE',  ( 0.000000000000000000, 0.9967269304714136968, 0.08084198211964954695 ) ) ;
#10313=CARTESIAN_POINT ( 'NONE',  ( -8.063330319165405768, -10.15233964170348457, 1.310587897985993733 ) ) ;
#10376=B_SPLINE_CURVE_WITH_KNOTS ( 'NONE', 3,
 ( #68290, #59692, #92607, #99706, #98223, #61195, #92114, #28731 ),
 .UNSPECIFIED., .F., .F.,
 ( 4, 2, 2, 4 ),
 ( 0.000000000000000000, 0.0003937098746455595455, 0.0007874197492911190911, 0.001574839498582238182 ),
 .UNSPECIFIED. ) ;
#10424=ADVANCED_FACE ( 'NONE', ( #37883 ), #42154, .F. ) ;
#10443=B_SPLINE_CURVE_WITH_KNOTS ( 'NONE', 3,
 ( #58760, #42056, #50159, #43541 ),
 .UNSPECIFIED., .F., .F.,
 ( 4, 4 ),
 ( 0.000000000000000000, 0.0004434240296263077972 ),
 .UNSPECIFIED. ) ;
#10539=CARTESIAN_POINT ( 'NONE',  ( 8.160000000000000142, 0.000000000000000000, 0.000000000000000000 ) ) ;
#10548=CARTESIAN_POINT ( 'NONE',  ( 8.160000000000000142, -10.65233964170348635, -1.621096496867198589 ) ) ;
#10597=EDGE_CURVE ( 'NONE', #68497, #62307, #22633, .T. ) ;
#10680=CARTESIAN_POINT ( 'NONE',  ( 8.160000000000000142, 8.793627758918228565, -2.994553991265763049 ) ) ;
#10697=FACE_OUTER_BOUND ( 'NONE', #88720, .T. ) ;
#10711=FACE_OUTER_BOUND ( 'NONE', #7136, .T. ) ;
#10720=ORIENTED_EDGE ( 'NONE', *, *, #1241, .T. ) ;
#10759=CIRCLE ( 'NONE', #85277, 20.00000000000000355 ) ;
#10878=ORIENTED_EDGE ( 'NONE', *, *, #76208, .T. ) ;
#10890=ORIENTED_EDGE ( 'NONE', *, *, #16225, .T. ) ;
#10891=EDGE_CURVE ( 'NONE', #53605, #68497, #28160, .T. ) ;
#10997=ORIENTED_EDGE ( 'NONE', *, *, #32029, .T. ) ;
#11065=DIRECTION ( 'NONE',  ( -1.000000000000000000, -0.000000000000000000, -0.000000000000000000 ) ) ;
#11111=ORIENTED_EDGE ( 'NONE', *, *, #6485, .F. ) ;
#11182=CARTESIAN_POINT ( 'NONE',  ( 8.160000000000000142, -10.15233964170348457, 0.003711184059992174607 ) ) ;
#11207=DIRECTION ( 'NONE',  ( 1.000000000000000000, -0.000000000000000000, 0.000000000000000000 ) ) ;
#11255=ORIENTED_EDGE ( 'NONE', *, *, #40684, .T. ) ;
#11256=CARTESIAN_POINT ( 'NONE',  ( 8.160000000000000142, -10.15233964170348457, 0.003711184059992174607 ) ) ;
#11303=DIRECTION ( 'NONE',  ( 0.000000000000000000, 0.000000000000000000, 1.000000000000000000 ) ) ;
#11306=CARTESIAN_POINT ( 'NONE',  ( 8.160000000000000142, -8.603846352786376883, -0.6978360589526751978 ) ) ;
#11322=CARTESIAN_POINT ( 'NONE',  ( -6.660000000000001030, -6.553980293839118509, 7.335060089566987962 ) ) ;
#11339=LINE ( 'NONE', #3739, #59736 ) ;
#11390=AXIS2_PLACEMENT_3D ( 'NONE', #57874, #74569, #81188 ) ;
#11506=AXIS2_PLACEMENT_3D ( 'NONE', #46493, #24146, #92651 ) ;
#11540=VERTEX_POINT ( 'NONE', #47144 ) ;
#11553=DIRECTION ( 'NONE',  ( 0.000000000000000000, -0.3081562241202470687, -0.9513357669802772199 ) ) ;
#11702=DIRECTION ( 'NONE',  ( 0.000000000000000000, 0.000000000000000000, -1.000000000000000000 ) ) ;
#11800=CARTESIAN_POINT ( 'NONE',  ( -8.160000000000000142, -10.15233964170348457, 0.003711184059992174607 ) ) ;
#11851=EDGE_CURVE ( 'NONE', #27461, #82473, #6451, .T. ) ;
#11938=DIRECTION ( 'NONE',  ( 0.000000000000000000, 0.000000000000000000, -1.000000000000000000 ) ) ;
#12136=ORIENTED_EDGE ( 'NONE', *, *, #91149, .F. ) ;
#12174=ORIENTED_EDGE ( 'NONE', *, *, #24907, .F. ) ;
#12230=ORIENTED_EDGE ( 'NONE', *, *, #47716, .F. ) ;
#12258=CYLINDRICAL_SURFACE ( 'NONE', #38416, 2.899999999999999911 ) ;
#12320=DIRECTION ( 'NONE',  ( 0.000000000000000000, 0.9967269304714136968, 0.08084198211964954695 ) ) ;
#12526=CARTESIAN_POINT ( 'NONE',  ( -8.160000000000000142, -10.65233964170348635, 1.628518864987183790 ) ) ;
#12555=LINE ( 'NONE', #88696, #55729 ) ;
#12561=ORIENTED_EDGE ( 'NONE', *, *, #20331, .F. ) ;
#12682=CIRCLE ( 'NONE', #53260, 20.00000000000000355 ) ;
#12698=CARTESIAN_POINT ( 'NONE',  ( -8.160000000000000142, -10.15233964170348457, 0.003711184059992174607 ) ) ;
#12713=CARTESIAN_POINT ( 'NONE',  ( 7.160000000000000142, -6.754662360505032659, 7.925641719537454222 ) ) ;
#12767=EDGE_CURVE ( 'NONE', #97595, #51586, #62499, .T. ) ;
#12780=CLOSED_SHELL ( 'NONE', ( #94564, #48137, #64114, #87577, #19854, #67713, #6787, #7043, #54379, #88561, #81574, #30448, #77872, #60883, #7909, #7963, #64305, #82317, #67653, #37429, #1159, #86121, #27203, #72171, #188, #59072, #6249, #65348, #78713, #15968, #40513, #38544, #14625, #83633, #5337, #63231, #61581, #26786, #93106, #14616, #20344, #85617, #16875, #55508, #58982, #16793, #80241, #29627, #19073, #78202, #80819, #80245, #27682, #14657, #30764, #60782, #83207, #82746, #20306, #58940, #10424, #26287, #856, #65132, #30973, #86299, #14500, #9953 ) ) ;
#12919=FACE_OUTER_BOUND ( 'NONE', #82011, .T. ) ;
#12978=ORIENTED_EDGE ( 'NONE', *, *, #12767, .T. ) ;
#13211=DIRECTION ( 'NONE',  ( 0.000000000000000000, 0.000000000000000000, -1.000000000000000000 ) ) ;
#13307=ORIENTED_EDGE ( 'NONE', *, *, #11851, .T. ) ;
#13329=VERTEX_POINT ( 'NONE', #79090 ) ;
#13333=EDGE_CURVE ( 'NONE', #11540, #45568, #67372, .T. ) ;
#13349=VERTEX_POINT ( 'NONE', #89590 ) ;
#13370=ORIENTED_EDGE ( 'NONE', *, *, #39723, .F. ) ;
#13436=DIRECTION ( 'NONE',  ( 0.000000000000000000, -1.000000000000000000, -1.020425574104004246E-16 ) ) ;
#13508=CARTESIAN_POINT ( 'NONE',  ( -8.160000000000000142, -10.15233964170348457, 0.003711184059992174607 ) ) ;
#13512=ORIENTED_EDGE ( 'NONE', *, *, #5196, .T. ) ;
#13539=VECTOR ( 'NONE', #72475, 1000.000000000000000 ) ;
#13858=ORIENTED_EDGE ( 'NONE', *, *, #99262, .T. ) ;
#13913=DIRECTION ( 'NONE',  ( -0.000000000000000000, 0.000000000000000000, 1.000000000000000000 ) ) ;
#14115=ORIENTED_EDGE ( 'NONE', *, *, #31121, .F. ) ;
#14194=VECTOR ( 'NONE', #93794, 1000.000000000000000 ) ;
#14297=FACE_OUTER_BOUND ( 'NONE', #71910, .T. ) ;
#14429=CARTESIAN_POINT ( 'NONE',  ( 8.160000000000000142, -6.754662360505033547, 8.925641719537455998 ) ) ;
#14436=DESIGN_CONTEXT ( 'detailed design', #59603, 'design' ) ;
#14448=CARTESIAN_POINT ( 'NONE',  ( 8.160000000000000142, 0.000000000000000000, 0.000000000000000000 ) ) ;
#14453=DIRECTION ( 'NONE',  ( 0.000000000000000000, 0.000000000000000000, -1.000000000000000000 ) ) ;
#14495=VERTEX_POINT ( 'NONE', #85728 ) ;
#14500=ADVANCED_FACE ( 'NONE', ( #70508 ), #94334, .T. ) ;
#14539=CIRCLE ( 'NONE', #8027, 1.699999999999999289 ) ;
#14571=( NAMED_UNIT ( * ) SI_UNIT ( $, .STERADIAN. ) SOLID_ANGLE_UNIT ( ) );
#14616=ADVANCED_FACE ( 'NONE', ( #56304, #42570 ), #87735, .F. ) ;
#14625=ADVANCED_FACE ( 'NONE', ( #18219 ), #88238, .F. ) ;
#14656=CARTESIAN_POINT ( 'NONE',  ( -8.160000000000000142, 0.000000000000000000, 0.000000000000000000 ) ) ;
#14657=ADVANCED_FACE ( 'NONE', ( #27330 ), #34941, .T. ) ;
#14867=ORIENTED_EDGE ( 'NONE', *, *, #53452, .T. ) ;
#14942=ORIENTED_EDGE ( 'NONE', *, *, #47111, .T. ) ;
#14970=CARTESIAN_POINT ( 'NONE',  ( 7.160000000000000142, 7.891155995661682354, 5.788828319098143993 ) ) ;
#15019=LINE ( 'NONE', #61225, #52196 ) ;
#15148=DIRECTION ( 'NONE',  ( 0.000000000000000000, -0.3081562241202474572, -0.9513357669802769978 ) ) ;
#15151=AXIS2_PLACEMENT_3D ( 'NONE', #47616, #15148, #68942 ) ;
#15298=CARTESIAN_POINT ( 'NONE',  ( -6.660000000000001030, 8.793627758918228565, -2.994553991265763049 ) ) ;
#15401=EDGE_CURVE ( 'NONE', #65066, #99147, #44650, .T. ) ;
#15501=ORIENTED_EDGE ( 'NONE', *, *, #33860, .F. ) ;
#15565=CARTESIAN_POINT ( 'NONE',  ( -6.660000000000001030, 2.939152317953647106E-16, -2.399999999999999911 ) ) ;
#15613=ORIENTED_EDGE ( 'NONE', *, *, #64449, .F. ) ;
#15664=CARTESIAN_POINT ( 'NONE',  ( 8.160000000000000142, -7.443174476472325551, 8.148664233019720982 ) ) ;
#15684=FACE_OUTER_BOUND ( 'NONE', #44579, .T. ) ;
#15811=CARTESIAN_POINT ( 'NONE',  ( -8.160000000000000142, -9.636585826567531043, 1.623587105904843231 ) ) ;
#15819=DIRECTION ( 'NONE',  ( 0.000000000000000000, -0.3081562241202474572, -0.9513357669802769978 ) ) ;
#15869=VECTOR ( 'NONE', #56572, 1000.000000000000000 ) ;
#15877=AXIS2_PLACEMENT_3D ( 'NONE', #52889, #7704, #83828 ) ;
#15968=ADVANCED_FACE ( 'NONE', ( #10711 ), #95442, .F. ) ;
#15979=DIRECTION ( 'NONE',  ( 0.000000000000000000, 0.000000000000000000, 1.000000000000000000 ) ) ;
#15993=ORIENTED_EDGE ( 'NONE', *, *, #47111, .F. ) ;
#16001=DIRECTION ( 'NONE',  ( -1.000000000000000000, 0.000000000000000000, 0.000000000000000000 ) ) ;
#16114=EDGE_LOOP ( 'NONE', ( #20571, #84913, #5885, #86273 ) ) ;
#16168=CIRCLE ( 'NONE', #29131, 2.399999999999999911 ) ;
#16211=VECTOR ( 'NONE', #43330, 1000.000000000000000 ) ;
#16225=EDGE_CURVE ( 'NONE', #60171, #99147, #77580, .T. ) ;
#16327=EDGE_CURVE ( 'NONE', #64237, #97633, #89841, .T. ) ;
#16359=EDGE_CURVE ( 'NONE', #92914, #31760, #55277, .T. ) ;
#16367=VERTEX_POINT ( 'NONE', #33929 ) ;
#16369=CARTESIAN_POINT ( 'NONE',  ( -6.660000000000001030, -10.77121780415746599, 1.154761385154455366 ) ) ;
#16446=CARTESIAN_POINT ( 'NONE',  ( -7.160000000000000142, 1.990213166801898970, 6.144159427248533589 ) ) ;
#16466=EDGE_LOOP ( 'NONE', ( #2551, #29329, #49200, #54175 ) ) ;
#16484=AXIS2_PLACEMENT_3D ( 'NONE', #38037, #76582, #31426 ) ;
#16565=SPHERICAL_SURFACE ( 'NONE', #5672, 1.000000000000000000 ) ;
#16593=AXIS2_PLACEMENT_3D ( 'NONE', #98752, #98249, #20135 ) ;
#16748=ORIENTED_EDGE ( 'NONE', *, *, #51155, .T. ) ;
#16793=ADVANCED_FACE ( 'NONE', ( #64282 ), #16565, .T. ) ;
#16798=CYLINDRICAL_SURFACE ( 'NONE', #22282, 1.000000000000000000 ) ;
#16835=DIRECTION ( 'NONE',  ( 0.000000000000000000, 0.000000000000000000, 1.000000000000000000 ) ) ;
#16875=ADVANCED_FACE ( 'NONE', ( #37167 ), #59022, .T. ) ;
#16922=LINE ( 'NONE', #72607, #53983 ) ;
#17010=CARTESIAN_POINT ( 'NONE',  ( 8.160000000000000142, -2.890508098367099432, -0.2344417481469836528 ) ) ;
#17227=DIRECTION ( 'NONE',  ( 0.000000000000000000, -0.8955258983741299916, -0.4450093991605204025 ) ) ;
#17331=CARTESIAN_POINT ( 'NONE',  ( 7.160000000000000142, -0.4583917923827244278, 5.886156785137588443 ) ) ;
#17424=CARTESIAN_POINT ( 'NONE',  ( -7.777949202540602514, -10.53666143673956768, 1.254198837351630402 ) ) ;
#17495=DIRECTION ( 'NONE',  ( -0.000000000000000000, 1.000000000000000000, 1.020425574104004246E-16 ) ) ;
#17612=CARTESIAN_POINT ( 'NONE',  ( 7.160000000000000142, -10.77121780415746599, 1.154761385154455366 ) ) ;
#17648=CIRCLE ( 'NONE', #97032, 2.399999999999999911 ) ;
#17655=FACE_OUTER_BOUND ( 'NONE', #93370, .T. ) ;
#17722=DIRECTION ( 'NONE',  ( 0.000000000000000000, 0.3081562241202474017, 0.9513357669802769978 ) ) ;
#17810=DIRECTION ( 'NONE',  ( 0.000000000000000000, 1.734723475976807094E-15, -1.000000000000000000 ) ) ;
#17830=CIRCLE ( 'NONE', #38820, 20.00000000000000000 ) ;
#17988=ORIENTED_EDGE ( 'NONE', *, *, #89143, .T. ) ;
#18008=DIRECTION ( 'NONE',  ( 0.000000000000000000, -0.000000000000000000, -1.000000000000000000 ) ) ;
#18023=CIRCLE ( 'NONE', #53671, 1.306876713926001354 ) ;
#18075=CIRCLE ( 'NONE', #97524, 1.306876713926001798 ) ;
#18215=DIRECTION ( 'NONE',  ( 0.000000000000000000, 0.000000000000000000, 1.000000000000000000 ) ) ;
#18219=FACE_OUTER_BOUND ( 'NONE', #16114, .T. ) ;
#18275=DIRECTION ( 'NONE',  ( 0.000000000000000000, 0.000000000000000000, -1.000000000000000000 ) ) ;
#18298=EDGE_LOOP ( 'NONE', ( #85616, #12978 ) ) ;
#18321=DIRECTION ( 'NONE',  ( -1.000000000000000000, -0.000000000000000000, -0.000000000000000000 ) ) ;
#18370=DIRECTION ( 'NONE',  ( -1.000000000000000000, 0.000000000000000000, -0.000000000000000000 ) ) ;
#18372=DIRECTION ( 'NONE',  ( -1.000000000000000000, -0.000000000000000000, -0.000000000000000000 ) ) ;
#18448=DIRECTION ( 'NONE',  ( -1.000000000000000000, 0.000000000000000000, 0.000000000000000000 ) ) ;
#18452=ORIENTED_EDGE ( 'NONE', *, *, #22090, .T. ) ;
#18503=DIRECTION ( 'NONE',  ( 0.000000000000000000, 1.084202172485504434E-16, -1.000000000000000000 ) ) ;
#18636=AXIS2_PLACEMENT_3D ( 'NONE', #56803, #80613, #95839 ) ;
#18717=CIRCLE ( 'NONE', #70517, 1.000000000000000000 ) ;
#18728=VERTEX_POINT ( 'NONE', #2592 ) ;
#18753=ORIENTED_EDGE ( 'NONE', *, *, #96329, .F. ) ;
#18774=DIRECTION ( 'NONE',  ( 0.000000000000000000, 0.000000000000000000, -1.000000000000000000 ) ) ;
#18812=CARTESIAN_POINT ( 'NONE',  ( -8.160000000000000142, 0.000000000000000000, 0.000000000000000000 ) ) ;
#18824=DIRECTION ( 'NONE',  ( 1.000000000000000000, 0.000000000000000000, 0.000000000000000000 ) ) ;
#18872=CARTESIAN_POINT ( 'NONE',  ( 8.160000000000000142, -6.754662360505033547, 7.925641719537454222 ) ) ;
#18890=ORIENTED_EDGE ( 'NONE', *, *, #60333, .T. ) ;
#18939=DIRECTION ( 'NONE',  ( 1.000000000000000000, -0.000000000000000000, 0.000000000000000000 ) ) ;
#18975=CARTESIAN_POINT ( 'NONE',  ( 6.660000000000001030, -10.15233964170348457, 0.003711184059992174607 ) ) ;
#18996=ORIENTED_EDGE ( 'NONE', *, *, #64377, .F. ) ;
#19073=ADVANCED_FACE ( 'NONE', ( #91948 ), #93948, .T. ) ;
#19137=CARTESIAN_POINT ( 'NONE',  ( -7.160000000000000142, -6.754662360505033547, 8.925641719537455998 ) ) ;
#19167=EDGE_CURVE ( 'NONE', #50221, #55102, #93439, .T. ) ;
#19248=CARTESIAN_POINT ( 'NONE',  ( 6.660000000000001030, 9.283009703645923594, -0.8121581124701985344 ) ) ;
#19331=ORIENTED_EDGE ( 'NONE', *, *, #58844, .T. ) ;
#19347=AXIS2_PLACEMENT_3D ( 'NONE', #87791, #39604, #23869 ) ;
#19439=DIRECTION ( 'NONE',  ( 1.000000000000000000, 0.000000000000000000, 0.000000000000000000 ) ) ;
#19543=CARTESIAN_POINT ( 'NONE',  ( 8.160000000000000142, 0.000000000000000000, 0.000000000000000000 ) ) ;
#19597=EDGE_LOOP ( 'NONE', ( #83847, #93460, #88627, #94093 ) ) ;
#19603=EDGE_LOOP ( 'NONE', ( #89596, #67862, #76236, #3148, #7226, #58296 ) ) ;
#19718=ORIENTED_EDGE ( 'NONE', *, *, #33860, .T. ) ;
#19772=FACE_OUTER_BOUND ( 'NONE', #114, .T. ) ;
#19777=VERTEX_POINT ( 'NONE', #36929 ) ;
#19800=CIRCLE ( 'NONE', #70002, 18.50000000000000000 ) ;
#19854=ADVANCED_FACE ( 'NONE', ( #7470 ), #62283, .T. ) ;
#19856=LINE ( 'NONE', #35607, #69150 ) ;
#19906=EDGE_CURVE ( 'NONE', #3020, #36632, #85598, .T. ) ;
#19981=CARTESIAN_POINT ( 'NONE',  ( -8.160000000000000142, -6.754662360505033547, 7.925641719537454222 ) ) ;
#20112=ORIENTED_EDGE ( 'NONE', *, *, #21897, .T. ) ;
#20118=EDGE_CURVE ( 'NONE', #63848, #93973, #69190, .T. ) ;
#20133=DIRECTION ( 'NONE',  ( 0.000000000000000000, 0.000000000000000000, 1.000000000000000000 ) ) ;
#20135=DIRECTION ( 'NONE',  ( 0.000000000000000000, 0.000000000000000000, 1.000000000000000000 ) ) ;
#20150=DIRECTION ( 'NONE',  ( 0.000000000000000000, 0.000000000000000000, -1.000000000000000000 ) ) ;
#20159=VECTOR ( 'NONE', #23292, 1000.000000000000000 ) ;
#20211=CARTESIAN_POINT ( 'NONE',  ( 8.160000000000000142, 2.888964624466060727, -0.2527516539682188590 ) ) ;
#20304=LINE ( 'NONE', #67018, #49952 ) ;
#20306=ADVANCED_FACE ( 'NONE', ( #57551 ), #49943, .T. ) ;
#20316=ORIENTED_EDGE ( 'NONE', *, *, #98598, .T. ) ;
#20331=EDGE_CURVE ( 'NONE', #80380, #53265, #96713, .T. ) ;
#20344=ADVANCED_FACE ( 'NONE', ( #88490 ), #79361, .T. ) ;
#20355=FACE_OUTER_BOUND ( 'NONE', #72153, .T. ) ;
#20377=AXIS2_PLACEMENT_3D ( 'NONE', #41286, #35179, #59902 ) ;
#20478=CARTESIAN_POINT ( 'NONE',  ( 7.160000000000000142, -6.754662360505034435, 7.925641719537454222 ) ) ;
#20552=EDGE_CURVE ( 'NONE', #21243, #48074, #38486, .T. ) ;
#20571=ORIENTED_EDGE ( 'NONE', *, *, #64121, .F. ) ;
#20598=CARTESIAN_POINT ( 'NONE',  ( -8.160000000000000142, 0.000000000000000000, 2.399999999999999911 ) ) ;
#20689=AXIS2_PLACEMENT_3D ( 'NONE', #70804, #26122, #18008 ) ;
#20729=VERTEX_POINT ( 'NONE', #49701 ) ;
#20788=LINE ( 'NONE', #77070, #26383 ) ;
#20849=ORIENTED_EDGE ( 'NONE', *, *, #69011, .T. ) ;
#20933=CIRCLE ( 'NONE', #38752, 1.000000000000000222 ) ;
#20974=DIRECTION ( 'NONE',  ( 0.000000000000000000, 0.000000000000000000, 1.000000000000000000 ) ) ;
#21087=DIRECTION ( 'NONE',  ( 0.000000000000000000, 0.000000000000000000, -1.000000000000000000 ) ) ;
#21243=VERTEX_POINT ( 'NONE', #84001 ) ;
#21267=AXIS2_PLACEMENT_3D ( 'NONE', #23507, #7802, #84426 ) ;
#21345=DIRECTION ( 'NONE',  ( -1.000000000000000000, 0.000000000000000000, -0.000000000000000000 ) ) ;
#21396=VECTOR ( 'NONE', #41794, 1000.000000000000000 ) ;
#21444=VECTOR ( 'NONE', #67222, 1000.000000000000000 ) ;
#21459=ORIENTED_EDGE ( 'NONE', *, *, #51643, .F. ) ;
#21471=EDGE_CURVE ( 'NONE', #56978, #19777, #96605, .T. ) ;
#21499=B_SPLINE_CURVE_WITH_KNOTS ( 'NONE', 3,
 ( #62344, #936, #31886, #76042, #76536, #62860 ),
 .UNSPECIFIED., .F., .F.,
 ( 4, 2, 4 ),
 ( 0.001160938631735150117, 0.001382550680209819645, 0.001604162728684488956 ),
 .UNSPECIFIED. ) ;
#21522=FACE_OUTER_BOUND ( 'NONE', #49072, .T. ) ;
#21559=EDGE_CURVE ( 'NONE', #71622, #64237, #74198, .T. ) ;
#21583=ORIENTED_EDGE ( 'NONE', *, *, #54719, .F. ) ;
#21595=CARTESIAN_POINT ( 'NONE',  ( -8.160000000000000142, -9.652339641703484574, -1.621096496867199033 ) ) ;
#21622=VERTEX_POINT ( 'NONE', #21958 ) ;
#21684=DIRECTION ( 'NONE',  ( 0.000000000000000000, 0.5747471426738535172, 0.8183310589170139648 ) ) ;
#21740=CYLINDRICAL_SURFACE ( 'NONE', #51493, 2.399999999999999911 ) ;
#21753=VECTOR ( 'NONE', #48587, 1000.000000000000000 ) ;
#21779=CARTESIAN_POINT ( 'NONE',  ( -7.160000000000000142, 7.891155995661682354, 5.788828319098143993 ) ) ;
#21785=DIRECTION ( 'NONE',  ( 0.000000000000000000, 0.000000000000000000, -1.000000000000000000 ) ) ;
#21879=LINE ( 'NONE', #6173, #36105 ) ;
#21897=EDGE_CURVE ( 'NONE', #64237, #60171, #72613, .T. ) ;
#21901=DIRECTION ( 'NONE',  ( 0.000000000000000000, 0.000000000000000000, -1.000000000000000000 ) ) ;
#21911=FACE_OUTER_BOUND ( 'NONE', #81536, .T. ) ;
#21958=CARTESIAN_POINT ( 'NONE',  ( -8.063330319165405768, -10.15233964170348457, 1.310587897985993733 ) ) ;
#21965=ORIENTED_EDGE ( 'NONE', *, *, #86675, .T. ) ;
#22069=ORIENTED_EDGE ( 'NONE', *, *, #290, .F. ) ;
#22090=EDGE_CURVE ( 'NONE', #31760, #78378, #51530, .T. ) ;
#22116=DIRECTION ( 'NONE',  ( -1.000000000000000000, 0.000000000000000000, 0.000000000000000000 ) ) ;
#22151=EDGE_CURVE ( 'NONE', #56978, #46703, #87158, .T. ) ;
#22168=EDGE_CURVE ( 'NONE', #87869, #18728, #96991, .T. ) ;
#22218=EDGE_CURVE ( 'NONE', #87928, #82473, #38553, .T. ) ;
#22263=DIRECTION ( 'NONE',  ( -1.000000000000000000, -0.000000000000000000, -0.000000000000000000 ) ) ;
#22269=LINE ( 'NONE', #68473, #72332 ) ;
#22282=AXIS2_PLACEMENT_3D ( 'NONE', #62999, #9692, #65011 ) ;
#22410=CARTESIAN_POINT ( 'NONE',  ( 6.660000000000001030, 9.283009703645923594, -0.8121581124701985344 ) ) ;
#22414=LINE ( 'NONE', #92436, #84235 ) ;
#22430=SHAPE_REPRESENTATION ( 'Locking Button_Varsay\X2\0131\X0\lan', ( #37391 ), #48843 ) ;
#22433=CARTESIAN_POINT ( 'NONE',  ( 7.160000000000000142, -7.572993419422048511, 8.500388862211309515 ) ) ;
#22502=CIRCLE ( 'NONE', #43612, 1.000000000000000000 ) ;
#22633=LINE ( 'NONE', #55115, #5319 ) ;
#22670=DIRECTION ( 'NONE',  ( 1.000000000000000000, -0.000000000000000000, 0.000000000000000000 ) ) ;
#22689=CARTESIAN_POINT ( 'NONE',  ( -8.160000000000000142, -2.890508098367099432, -0.2344417481469836528 ) ) ;
#22697=ORIENTED_EDGE ( 'NONE', *, *, #21559, .T. ) ;
#22718=ORIENTED_EDGE ( 'NONE', *, *, #73861, .F. ) ;
#22771=CARTESIAN_POINT ( 'NONE',  ( -11.16000000000000014, -9.652339641703484574, 1.628518864987183790 ) ) ;
#22805=EDGE_CURVE ( 'NONE', #76784, #81299, #97568, .T. ) ;
#22875=VERTEX_POINT ( 'NONE', #84606 ) ;
#23013=CARTESIAN_POINT ( 'NONE',  ( 8.160000000000000142, -6.927494035009244411E-16, 6.788828319098143105 ) ) ;
#23058=AXIS2_PLACEMENT_3D ( 'NONE', #89195, #33397, #64389 ) ;
#23084=AXIS2_PLACEMENT_3D ( 'NONE', #76918, #31256, #812 ) ;
#23098=ORIENTED_EDGE ( 'NONE', *, *, #75938, .F. ) ;
#23165=CIRCLE ( 'NONE', #79895, 19.00000000000000000 ) ;
#23254=AXIS2_PLACEMENT_3D ( 'NONE', #87415, #63605, #95031 ) ;
#23292=DIRECTION ( 'NONE',  ( 0.000000000000000000, 0.9513357669802769978, -0.3081562241202474572 ) ) ;
#23332=ORIENTED_EDGE ( 'NONE', *, *, #84921, .F. ) ;
#23406=CARTESIAN_POINT ( 'NONE',  ( -6.660000000000001030, 8.793627758918228565, -2.994553991265763049 ) ) ;
#23425=ORIENTED_EDGE ( 'NONE', *, *, #81428, .F. ) ;
#23441=ORIENTED_EDGE ( 'NONE', *, *, #84921, .T. ) ;
#23481=VECTOR ( 'NONE', #72787, 1000.000000000000000 ) ;
#23501=PLANE ( 'NONE',  #57642 ) ;
#23507=CARTESIAN_POINT ( 'NONE',  ( -7.160000000000000142, -9.123836073446797812, -2.666350264951732552 ) ) ;
#23511=EDGE_LOOP ( 'NONE', ( #69554, #14867, #1313, #14115, #12561 ) ) ;
#23523=DIRECTION ( 'NONE',  ( 0.000000000000000000, 0.000000000000000000, 1.000000000000000000 ) ) ;
#23538=AXIS2_PLACEMENT_3D ( 'NONE', #73018, #89230, #72517 ) ;
#23588=CYLINDRICAL_SURFACE ( 'NONE', #46384, 2.899999999999999911 ) ;
#23601=CARTESIAN_POINT ( 'NONE',  ( 8.133973695506851342, 10.05415566027042829, -0.8796246415986995748 ) ) ;
#23624=CARTESIAN_POINT ( 'NONE',  ( 8.160000000000000142, -2.890508098367099432, -0.2344417481469836528 ) ) ;
#23869=DIRECTION ( 'NONE',  ( 0.000000000000000000, 0.3081562241202472352, 0.9513357669802769978 ) ) ;
#23919=DIRECTION ( 'NONE',  ( 0.000000000000000000, 0.08084198211964954695, -0.9967269304714136968 ) ) ;
#23925=EDGE_CURVE ( 'NONE', #3797, #45450, #7499, .T. ) ;
#23993=DIRECTION ( 'NONE',  ( -1.000000000000000000, 0.000000000000000000, 0.000000000000000000 ) ) ;
#24043=AXIS2_PLACEMENT_3D ( 'NONE', #15298, #84313, #30023 ) ;
#24069=AXIS2_PLACEMENT_3D ( 'NONE', #18812, #26443, #71616 ) ;
#24129=CARTESIAN_POINT ( 'NONE',  ( 8.160000000000000142, -10.15233964170348457, 0.003711184059992174607 ) ) ;
#24130=EDGE_CURVE ( 'NONE', #98627, #63848, #71920, .T. ) ;
#24146=DIRECTION ( 'NONE',  ( 1.000000000000000000, -0.000000000000000000, -0.000000000000000000 ) ) ;
#24213=ORIENTED_EDGE ( 'NONE', *, *, #99155, .F. ) ;
#24214=ORIENTED_EDGE ( 'NONE', *, *, #56843, .F. ) ;
#24229=DIRECTION ( 'NONE',  ( 0.000000000000000000, 0.000000000000000000, 1.000000000000000000 ) ) ;
#24329=ORIENTED_EDGE ( 'NONE', *, *, #72565, .F. ) ;
#24558=ORIENTED_EDGE ( 'NONE', *, *, #43157, .T. ) ;
#24639=CYLINDRICAL_SURFACE ( 'NONE', #11506, 1.699999999999999289 ) ;
#24718=CARTESIAN_POINT ( 'NONE',  ( -8.160000000000000142, -10.65233964170348635, -1.621096496867198589 ) ) ;
#24854=DIRECTION ( 'NONE',  ( 1.000000000000000000, 0.000000000000000000, 0.000000000000000000 ) ) ;
#24907=EDGE_CURVE ( 'NONE', #87025, #55690, #19856, .T. ) ;
#24909=EDGE_CURVE ( 'NONE', #1499, #87928, #25415, .T. ) ;
#24942=DIRECTION ( 'NONE',  ( -1.000000000000000000, 0.000000000000000000, 0.000000000000000000 ) ) ;
#25126=DIRECTION ( 'NONE',  ( 0.000000000000000000, 1.000000000000000000, 1.020425574104004246E-16 ) ) ;
#25154=AXIS2_PLACEMENT_3D ( 'NONE', #42072, #73506, #49684 ) ;
#25213=ORIENTED_EDGE ( 'NONE', *, *, #10597, .F. ) ;
#25378=CIRCLE ( 'NONE', #82098, 1.306876713926001354 ) ;
#25415=CIRCLE ( 'NONE', #95086, 1.000000000000000000 ) ;
#25417=DIRECTION ( 'NONE',  ( 0.000000000000000000, 1.000000000000000000, 1.020425574104004246E-16 ) ) ;
#25554=EDGE_LOOP ( 'NONE', ( #8282, #88862, #68588 ) ) ;
#25563=ORIENTED_EDGE ( 'NONE', *, *, #68630, .T. ) ;
#25612=AXIS2_PLACEMENT_3D ( 'NONE', #72733, #65637, #79326 ) ;
#25741=ORIENTED_EDGE ( 'NONE', *, *, #5143, .F. ) ;
#25747=ORIENTED_EDGE ( 'NONE', *, *, #13333, .F. ) ;
#25919=CARTESIAN_POINT ( 'NONE',  ( 8.160000000000000142, 7.891155995661682354, 5.788828319098143105 ) ) ;
#25929=CARTESIAN_POINT ( 'NONE',  ( 8.160000000000000142, -9.123836073446797812, -2.666350264951732552 ) ) ;
#25943=CIRCLE ( 'NONE', #58410, 18.50000000000000355 ) ;
#25948=DIRECTION ( 'NONE',  ( 0.000000000000000000, 0.9513357669802769978, -0.3081562241202473462 ) ) ;
#26012=DIRECTION ( 'NONE',  ( 0.000000000000000000, 0.000000000000000000, -1.000000000000000000 ) ) ;
#26122=DIRECTION ( 'NONE',  ( 0.000000000000000000, -1.000000000000000000, 0.000000000000000000 ) ) ;
#26145=ORIENTED_EDGE ( 'NONE', *, *, #33154, .F. ) ;
#26215=ORIENTED_EDGE ( 'NONE', *, *, #38891, .F. ) ;
#26221=ORIENTED_EDGE ( 'NONE', *, *, #27316, .T. ) ;
#26273=EDGE_LOOP ( 'NONE', ( #68652, #21583, #9120, #77837 ) ) ;
#26287=ADVANCED_FACE ( 'NONE', ( #88028 ), #95637, .F. ) ;
#26319=VECTOR ( 'NONE', #54446, 1000.000000000000000 ) ;
#26321=VERTEX_POINT ( 'NONE', #40842 ) ;
#26383=VECTOR ( 'NONE', #38023, 1000.000000000000000 ) ;
#26398=EDGE_CURVE ( 'NONE', #31972, #76784, #39842, .T. ) ;
#26443=DIRECTION ( 'NONE',  ( -1.000000000000000000, 0.000000000000000000, 0.000000000000000000 ) ) ;
#26498=DIRECTION ( 'NONE',  ( 0.000000000000000000, 0.000000000000000000, 1.000000000000000000 ) ) ;
#26541=DIRECTION ( 'NONE',  ( -1.000000000000000000, 0.000000000000000000, 0.000000000000000000 ) ) ;
#26546=CARTESIAN_POINT ( 'NONE',  ( -7.847517764308983956, -10.47139188923011233, 1.273303694910093986 ) ) ;
#26558=CARTESIAN_POINT ( 'NONE',  ( -8.160000000000000142, -0.1502355682624769706, 6.837492552117866218 ) ) ;
#26569=CARTESIAN_POINT ( 'NONE',  ( 6.660000000000001030, -10.15233964170348457, 0.003711184059992174607 ) ) ;
#26578=ORIENTED_EDGE ( 'NONE', *, *, #24909, .F. ) ;
#26606=VERTEX_POINT ( 'NONE', #66712 ) ;
#26693=CARTESIAN_POINT ( 'NONE',  ( 6.660000000000001030, 0.000000000000000000, 0.000000000000000000 ) ) ;
#26700=CARTESIAN_POINT ( 'NONE',  ( 11.16000000000000014, -10.65233964170348635, 1.628518864987183790 ) ) ;
#26709=ORIENTED_EDGE ( 'NONE', *, *, #13333, .T. ) ;
#26786=ADVANCED_FACE ( 'NONE', ( #4552 ), #21740, .F. ) ;
#26791=DIRECTION ( 'NONE',  ( -1.000000000000000000, -0.000000000000000000, -0.000000000000000000 ) ) ;
#26890=ORIENTED_EDGE ( 'NONE', *, *, #81394, .T. ) ;
#26914=VERTEX_POINT ( 'NONE', #35497 ) ;
#26955=CARTESIAN_POINT ( 'NONE',  ( 6.660000000000001030, -10.77121780415746599, 1.154761385154455366 ) ) ;
#27043=AXIS2_PLACEMENT_3D ( 'NONE', #55676, #7977, #48052 ) ;
#27047=PLANE ( 'NONE',  #75910 ) ;
#27053=AXIS2_PLACEMENT_3D ( 'NONE', #73676, #59962, #50847 ) ;
#27087=DIRECTION ( 'NONE',  ( 0.000000000000000000, 0.000000000000000000, -1.000000000000000000 ) ) ;
#27194=DIRECTION ( 'NONE',  ( -1.000000000000000000, 0.000000000000000000, 0.000000000000000000 ) ) ;
#27203=ADVANCED_FACE ( 'NONE', ( #80044 ), #3444, .T. ) ;
#27239=VERTEX_POINT ( 'NONE', #19137 ) ;
#27273=CIRCLE ( 'NONE', #67767, 18.50000000000000000 ) ;
#27316=EDGE_CURVE ( 'NONE', #98627, #97595, #44994, .T. ) ;
#27330=FACE_OUTER_BOUND ( 'NONE', #5249, .T. ) ;
#27449=EDGE_CURVE ( 'NONE', #71622, #97633, #78414, .T. ) ;
#27461=VERTEX_POINT ( 'NONE', #84035 ) ;
#27462=EDGE_CURVE ( 'NONE', #76784, #54393, #61064, .T. ) ;
#27490=CARTESIAN_POINT ( 'NONE',  ( -8.160000000000000142, -9.652339641703484574, -1.621096496867199033 ) ) ;
#27508=CARTESIAN_POINT ( 'NONE',  ( 6.660000000000001030, -10.15233964170348457, -1.303165529866009420 ) ) ;
#27510=DIRECTION ( 'NONE',  ( 0.000000000000000000, 0.000000000000000000, 1.000000000000000000 ) ) ;
#27527=AXIS2_PLACEMENT_3D ( 'NONE', #80063, #41508, #72463 ) ;
#27540=VECTOR ( 'NONE', #91259, 1000.000000000000000 ) ;
#27605=LINE ( 'NONE', #59056, #69836 ) ;
#27682=ADVANCED_FACE ( 'NONE', ( #79416 ), #79918, .T. ) ;
#27706=DIRECTION ( 'NONE',  ( -1.000000000000000000, 0.000000000000000000, -0.000000000000000000 ) ) ;
#27753=DIRECTION ( 'NONE',  ( -1.000000000000000000, 0.000000000000000000, 0.000000000000000000 ) ) ;
#27970=EDGE_LOOP ( 'NONE', ( #3260, #93929, #69890, #15993 ) ) ;
#27971=ORIENTED_EDGE ( 'NONE', *, *, #89655, .T. ) ;
#28025=DIRECTION ( 'NONE',  ( 0.000000000000000000, 0.000000000000000000, 1.000000000000000000 ) ) ;
#28040=ORIENTED_EDGE ( 'NONE', *, *, #24130, .F. ) ;
#28139=EDGE_CURVE ( 'NONE', #46936, #47734, #67586, .T. ) ;
#28160=LINE ( 'NONE', #83424, #7219 ) ;
#28169=DIRECTION ( 'NONE',  ( 1.000000000000000000, -0.000000000000000000, -0.000000000000000000 ) ) ;
#28277=AXIS2_PLACEMENT_3D ( 'NONE', #25929, #18321, #49291 ) ;
#28288=CARTESIAN_POINT ( 'NONE',  ( 8.160000000000000142, 8.793627758918228565, -2.994553991265763049 ) ) ;
#28385=VECTOR ( 'NONE', #39650, 1000.000000000000000 ) ;
#28425=EDGE_LOOP ( 'NONE', ( #72700, #74572, #72563, #23425, #50165, #99968, #34722 ) ) ;
#28502=EDGE_CURVE ( 'NONE', #78378, #51347, #57962, .T. ) ;
#28557=VECTOR ( 'NONE', #71287, 1000.000000000000000 ) ;
#28681=AXIS2_PLACEMENT_3D ( 'NONE', #40368, #25126, #56105 ) ;
#28731=CARTESIAN_POINT ( 'NONE',  ( -7.160000000000000142, 10.80195425911416507, -0.9450485415980990345 ) ) ;
#28854=AXIS2_PLACEMENT_3D ( 'NONE', #32084, #63060, #68661 ) ;
#28889=LINE ( 'NONE', #14656, #6376 ) ;
#28932=FACE_OUTER_BOUND ( 'NONE', #36599, .T. ) ;
#28974=AXIS2_PLACEMENT_3D ( 'NONE', #86630, #31852, #24229 ) ;
#28976=ORIENTED_EDGE ( 'NONE', *, *, #82307, .F. ) ;
#28992=AXIS2_PLACEMENT_3D ( 'NONE', #36419, #36918, #98304 ) ;
#29059=EDGE_CURVE ( 'NONE', #61839, #62307, #96768, .T. ) ;
#29092=DIRECTION ( 'NONE',  ( 9.210644184508402939E-16, 0.5747471426738538502, 0.8183310589170136318 ) ) ;
#29131=AXIS2_PLACEMENT_3D ( 'NONE', #42256, #74665, #97508 ) ;
#29206=TOROIDAL_SURFACE ( 'NONE', #1621, 2.000000000000000000, 1.000000000000000000 ) ;
#29284=CARTESIAN_POINT ( 'NONE',  ( -8.160000000000000142, 7.891155995661682354, 6.788828319098143993 ) ) ;
#29329=ORIENTED_EDGE ( 'NONE', *, *, #38891, .T. ) ;
#29363=ORIENTED_EDGE ( 'NONE', *, *, #86675, .F. ) ;
#29371=CARTESIAN_POINT ( 'NONE',  ( -7.160000000000000142, 8.793627758918228565, -2.994553991265763049 ) ) ;
#29415=ORIENTED_EDGE ( 'NONE', *, *, #55916, .T. ) ;
#29458=DIRECTION ( 'NONE',  ( -1.000000000000000000, 0.000000000000000000, 0.000000000000000000 ) ) ;
#29464=DIRECTION ( 'NONE',  ( 0.000000000000000000, 0.000000000000000000, 1.000000000000000000 ) ) ;
#29478=ORIENTED_EDGE ( 'NONE', *, *, #2896, .T. ) ;
#29525=DIRECTION ( 'NONE',  ( 0.000000000000000000, 0.000000000000000000, -1.000000000000000000 ) ) ;
#29568=PRODUCT_DEFINITION ( 'UNKNOWN', '', #55421, #14436 ) ;
#29615=DIRECTION ( 'NONE',  ( 1.000000000000000000, -0.000000000000000000, -0.000000000000000000 ) ) ;
#29627=ADVANCED_FACE ( 'NONE', ( #10697 ), #16798, .F. ) ;
#29773=CARTESIAN_POINT ( 'NONE',  ( -8.160000000000000142, 9.789768006247301813, -0.8564937190954607926 ) ) ;
#29833=ORIENTED_EDGE ( 'NONE', *, *, #19167, .F. ) ;
#29862=EDGE_CURVE ( 'NONE', #62319, #27239, #31793, .T. ) ;
#29877=CARTESIAN_POINT ( 'NONE',  ( 8.160000000000000142, -6.446506136384787311, 8.876977486517731109 ) ) ;
#29885=DIRECTION ( 'NONE',  ( 0.000000000000000000, 0.9961946980917453232, -0.08715574274766167695 ) ) ;
#29959=VERTEX_POINT ( 'NONE', #22771 ) ;
#30010=ORIENTED_EDGE ( 'NONE', *, *, #67672, .T. ) ;
#30023=DIRECTION ( 'NONE',  ( 0.000000000000000000, 0.000000000000000000, -1.000000000000000000 ) ) ;
#30087=AXIS2_PLACEMENT_3D ( 'NONE', #26569, #19439, #73242 ) ;
#30111=CARTESIAN_POINT ( 'NONE',  ( 7.160000000000000142, 8.793627758918228565, -2.994553991265763049 ) ) ;
#30236=CIRCLE ( 'NONE', #35106, 2.899999999999999911 ) ;
#30278=EDGE_CURVE ( 'NONE', #16367, #64045, #7890, .T. ) ;
#30360=ORIENTED_EDGE ( 'NONE', *, *, #69460, .F. ) ;
#30430=CIRCLE ( 'NONE', #59639, 1.699999999999999289 ) ;
#30448=ADVANCED_FACE ( 'NONE', ( #56123 ), #24639, .T. ) ;
#30485=ORIENTED_EDGE ( 'NONE', *, *, #22090, .F. ) ;
#30525=EDGE_CURVE ( 'NONE', #7384, #31760, #43959, .T. ) ;
#30577=ORIENTED_EDGE ( 'NONE', *, *, #62022, .T. ) ;
#30652=DIRECTION ( 'NONE',  ( 0.000000000000000000, 1.000000000000000000, 1.020425574104004246E-16 ) ) ;
#30712=ORIENTED_EDGE ( 'NONE', *, *, #36887, .T. ) ;
#30764=ADVANCED_FACE ( 'NONE', ( #86431 ), #3424, .T. ) ;
#30848=ORIENTED_EDGE ( 'NONE', *, *, #62590, .T. ) ;
#30866=ORIENTED_EDGE ( 'NONE', *, *, #5648, .T. ) ;
#30900=FACE_OUTER_BOUND ( 'NONE', #46852, .T. ) ;
#30973=ADVANCED_FACE ( 'NONE', ( #79810 ), #81319, .T. ) ;
#30975=ORIENTED_EDGE ( 'NONE', *, *, #54716, .F. ) ;
#30991=DIRECTION ( 'NONE',  ( 0.000000000000000000, 0.000000000000000000, 1.000000000000000000 ) ) ;
#31092=ORIENTED_EDGE ( 'NONE', *, *, #10077, .T. ) ;
#31111=ORIENTED_EDGE ( 'NONE', *, *, #33058, .T. ) ;
#31121=EDGE_CURVE ( 'NONE', #53265, #81299, #18023, .T. ) ;
#31212=FACE_OUTER_BOUND ( 'NONE', #27970, .T. ) ;
#31256=DIRECTION ( 'NONE',  ( 1.000000000000000000, -0.000000000000000000, 0.000000000000000000 ) ) ;
#31296=SHAPE_REPRESENTATION_RELATIONSHIP ( 'NONE' , 'NONE' ,  #22430, #48872 ) ;
#31358=EDGE_CURVE ( 'NONE', #5872, #82135, #88700, .T. ) ;
#31366=ORIENTED_EDGE ( 'NONE', *, *, #16359, .F. ) ;
#31426=DIRECTION ( 'NONE',  ( 0.000000000000000000, 1.734723475976807094E-15, 1.000000000000000000 ) ) ;
#31474=CIRCLE ( 'NONE', #96310, 1.000000000000000000 ) ;
#31601=VERTEX_POINT ( 'NONE', #93168 ) ;
#31685=VERTEX_POINT ( 'NONE', #9945 ) ;
#31706=EDGE_LOOP ( 'NONE', ( #85336, #20849, #3924, #13858 ) ) ;
#31743=PLANE ( 'NONE',  #53791 ) ;
#31750=DIRECTION ( 'NONE',  ( 0.000000000000000000, 0.000000000000000000, 1.000000000000000000 ) ) ;
#31755=AXIS2_PLACEMENT_3D ( 'NONE', #63590, #23993, #87401 ) ;
#31758=AXIS2_PLACEMENT_3D ( 'NONE', #53005, #52499, #75815 ) ;
#31759=AXIS2_PLACEMENT_3D ( 'NONE', #82774, #44229, #44723 ) ;
#31760=VERTEX_POINT ( 'NONE', #95187 ) ;
#31782=CARTESIAN_POINT ( 'NONE',  ( 8.160000000000000142, -9.123836073446797812, -2.666350264951732552 ) ) ;
#31793=CIRCLE ( 'NONE', #35283, 1.000000000000000888 ) ;
#31852=DIRECTION ( 'NONE',  ( -1.000000000000000000, 0.000000000000000000, 0.000000000000000000 ) ) ;
#31862=ORIENTED_EDGE ( 'NONE', *, *, #32762, .F. ) ;
#31870=VECTOR ( 'NONE', #8000, 1000.000000000000114 ) ;
#31886=CARTESIAN_POINT ( 'NONE',  ( -8.119068529101312492, -10.01380310104339344, 1.305235352931652715 ) ) ;
#31972=VERTEX_POINT ( 'NONE', #92057 ) ;
#32005=AXIS2_PLACEMENT_3D ( 'NONE', #73577, #88807, #18774 ) ;
#32029=EDGE_CURVE ( 'NONE', #32857, #27239, #44906, .T. ) ;
#32075=EDGE_LOOP ( 'NONE', ( #29833, #53034, #30712, #77616, #38579, #74501, #79789, #30975 ) ) ;
#32084=CARTESIAN_POINT ( 'NONE',  ( -8.160000000000000142, 8.793627758918228565, -2.994553991265763049 ) ) ;
#32094=LINE ( 'NONE', #16369, #26319 ) ;
#32097=ORIENTED_EDGE ( 'NONE', *, *, #43162, .T. ) ;
#32243=ORIENTED_EDGE ( 'NONE', *, *, #60074, .F. ) ;
#32279=DIRECTION ( 'NONE',  ( -1.000000000000000000, 0.000000000000000000, -0.000000000000000000 ) ) ;
#32290=EDGE_CURVE ( 'NONE', #39981, #56283, #97057, .T. ) ;
#32379=FACE_OUTER_BOUND ( 'NONE', #49060, .T. ) ;
#32447=VECTOR ( 'NONE', #29458, 1000.000000000000000 ) ;
#32550=CARTESIAN_POINT ( 'NONE',  ( -6.660000000000001030, 2.888964624466060727, -0.2527516539682188590 ) ) ;
#32644=ORIENTED_EDGE ( 'NONE', *, *, #58844, .F. ) ;
#32719=CIRCLE ( 'NONE', #16484, 1.000000000000000000 ) ;
#32762=EDGE_CURVE ( 'NONE', #1499, #48074, #2113, .T. ) ;
#32765=EDGE_LOOP ( 'NONE', ( #77250, #21459, #84152, #12230 ) ) ;
#32857=VERTEX_POINT ( 'NONE', #35053 ) ;
#32869=EDGE_LOOP ( 'NONE', ( #55047, #2983, #24214, #88159, #37870, #48295, #63047 ) ) ;
#33048=CARTESIAN_POINT ( 'NONE',  ( 8.160000000000000142, 8.786681894035815787, 6.233837718258663507 ) ) ;
#33058=EDGE_CURVE ( 'NONE', #46936, #55690, #58889, .T. ) ;
#33125=DIRECTION ( 'NONE',  ( -1.000000000000000000, 0.000000000000000000, -0.000000000000000000 ) ) ;
#33154=EDGE_CURVE ( 'NONE', #1499, #82473, #32719, .T. ) ;
#33230=CARTESIAN_POINT ( 'NONE',  ( 8.160000000000000142, -2.191226316053958875E-18, 2.701633758479787833E-17 ) ) ;
#33276=DIRECTION ( 'NONE',  ( -8.251522442585435191E-16, 0.9513357669802772199, -0.3081562241202470687 ) ) ;
#33397=DIRECTION ( 'NONE',  ( 1.000000000000000000, -0.000000000000000000, 0.000000000000000000 ) ) ;
#33418=DIRECTION ( 'NONE',  ( 1.000000000000000000, -0.000000000000000000, -0.000000000000000000 ) ) ;
#33533=DIRECTION ( 'NONE',  ( 0.000000000000000000, 1.020425574104004246E-16, -1.000000000000000000 ) ) ;
#33593=ORIENTED_EDGE ( 'NONE', *, *, #77273, .T. ) ;
#33860=EDGE_CURVE ( 'NONE', #50489, #41964, #92330, .T. ) ;
#33862=CARTESIAN_POINT ( 'NONE',  ( 7.160000000000000142, 7.891155995661684130, 5.788828319098143993 ) ) ;
#33869=EDGE_CURVE ( 'NONE', #70921, #76784, #14539, .T. ) ;
#33918=VERTEX_POINT ( 'NONE', #79056 ) ;
#33929=CARTESIAN_POINT ( 'NONE',  ( 6.660000000000001030, 2.888964624466060727, -0.2527516539682188035 ) ) ;
#33960=CARTESIAN_POINT ( 'NONE',  ( 6.660000000000001030, -2.890508098367099432, -0.2344417481469836528 ) ) ;
#34029=CARTESIAN_POINT ( 'NONE',  ( -8.160000000000000142, -10.15233964170348457, -1.303165529866009420 ) ) ;
#34043=ORIENTED_EDGE ( 'NONE', *, *, #34135, .F. ) ;
#34057=DIRECTION ( 'NONE',  ( 1.000000000000000000, 0.000000000000000000, 0.000000000000000000 ) ) ;
#34079=ORIENTED_EDGE ( 'NONE', *, *, #36890, .F. ) ;
#34109=EDGE_LOOP ( 'NONE', ( #18890, #44846, #72926, #24213 ) ) ;
#34135=EDGE_CURVE ( 'NONE', #78378, #51347, #58238, .T. ) ;
#34163=MECHANICAL_CONTEXT ( 'NONE', #4487, 'mechanical' ) ;
#34217=DIRECTION ( 'NONE',  ( 0.000000000000000000, 0.000000000000000000, -1.000000000000000000 ) ) ;
#34236=EDGE_CURVE ( 'NONE', #87928, #82230, #51862, .T. ) ;
#34237=ORIENTED_EDGE ( 'NONE', *, *, #15401, .T. ) ;
#34305=DIRECTION ( 'NONE',  ( 0.000000000000000000, 0.000000000000000000, 1.000000000000000000 ) ) ;
#34366=SPHERICAL_SURFACE ( 'NONE', #9215, 1.000000000000000000 ) ;
#34385=LINE ( 'NONE', #64866, #79462 ) ;
#34448=CIRCLE ( 'NONE', #81461, 1.000000000000000000 ) ;
#34550=CARTESIAN_POINT ( 'NONE',  ( 7.160000000000000142, 0.1579206558577706254, 7.788828319098143105 ) ) ;
#34638=DIRECTION ( 'NONE',  ( -1.000000000000000000, -0.000000000000000000, -0.000000000000000000 ) ) ;
#34658=VERTEX_POINT ( 'NONE', #20598 ) ;
#34663=FACE_OUTER_BOUND ( 'NONE', #50092, .T. ) ;
#34677=DIRECTION ( 'NONE',  ( 0.000000000000000000, 0.000000000000000000, -1.000000000000000000 ) ) ;
#34708=ORIENTED_EDGE ( 'NONE', *, *, #66892, .T. ) ;
#34722=ORIENTED_EDGE ( 'NONE', *, *, #42551, .F. ) ;
#34752=ORIENTED_EDGE ( 'NONE', *, *, #10891, .T. ) ;
#34872=ORIENTED_EDGE ( 'NONE', *, *, #52923, .T. ) ;
#34916=CARTESIAN_POINT ( 'NONE',  ( -8.160000000000000142, 8.793627758918228565, -2.994553991265763049 ) ) ;
#34939=EDGE_CURVE ( 'NONE', #40450, #5350, #4760, .T. ) ;
#34941=CYLINDRICAL_SURFACE ( 'NONE', #25154, 1.000000000000000000 ) ;
#34954=LINE ( 'NONE', #20211, #55147 ) ;
#34970=ORIENTED_EDGE ( 'NONE', *, *, #69635, .F. ) ;
#35053=CARTESIAN_POINT ( 'NONE',  ( 7.160000000000000142, -6.754662360505033547, 8.925641719537455998 ) ) ;
#35106=AXIS2_PLACEMENT_3D ( 'NONE', #26693, #27194, #34305 ) ;
#35133=ORIENTED_EDGE ( 'NONE', *, *, #49216, .T. ) ;
#35179=DIRECTION ( 'NONE',  ( 1.000000000000000000, 0.000000000000000000, 0.000000000000000000 ) ) ;
#35224=AXIS2_PLACEMENT_3D ( 'NONE', #6551, #36998, #89793 ) ;
#35283=AXIS2_PLACEMENT_3D ( 'NONE', #61872, #92797, #37022 ) ;
#35323=DIRECTION ( 'NONE',  ( 0.000000000000000000, 3.563215788492900483E-15, -1.000000000000000000 ) ) ;
#35389=AXIS2_PLACEMENT_3D ( 'NONE', #58892, #3612, #11702 ) ;
#35400=CARTESIAN_POINT ( 'NONE',  ( 8.160000000000000142, -9.636585826567532820, 1.623587105904843675 ) ) ;
#35407=CARTESIAN_POINT ( 'NONE',  ( -6.660000000000001030, 7.578413286920094194, 5.288828319098143105 ) ) ;
#35413=CARTESIAN_POINT ( 'NONE',  ( 7.160000000000000142, -6.754662360505033547, 7.925641719537452445 ) ) ;
#35443=CARTESIAN_POINT ( 'NONE',  ( 7.160000000000000142, 0.1579206558577708475, 5.788828319098143105 ) ) ;
#35497=CARTESIAN_POINT ( 'NONE',  ( -7.160000000000000142, -6.446506136384785535, 8.876977486517731109 ) ) ;
#35588=TOROIDAL_SURFACE ( 'NONE', #92293, 19.00000000000000355, 1.000000000000000000 ) ;
#35607=CARTESIAN_POINT ( 'NONE',  ( 6.660000000000001030, -9.572916487583196243, -0.7764348688322058045 ) ) ;
#35727=VECTOR ( 'NONE', #94248, 1000.000000000000000 ) ;
#36062=DIRECTION ( 'NONE',  ( 0.000000000000000000, 0.000000000000000000, -1.000000000000000000 ) ) ;
#36098=VERTEX_POINT ( 'NONE', #5769 ) ;
#36105=VECTOR ( 'NONE', #76663, 1000.000000000000000 ) ;
#36147=CIRCLE ( 'NONE', #83139, 19.00000000000000000 ) ;
#36251=ORIENTED_EDGE ( 'NONE', *, *, #49557, .T. ) ;
#36284=DIRECTION ( 'NONE',  ( 0.000000000000000000, 0.000000000000000000, -1.000000000000000000 ) ) ;
#36416=CARTESIAN_POINT ( 'NONE',  ( -8.160000000000000142, 0.000000000000000000, 0.000000000000000000 ) ) ;
#36419=CARTESIAN_POINT ( 'NONE',  ( 8.160000000000000142, -10.15233964170348457, 0.003711184059992174607 ) ) ;
#36504=CARTESIAN_POINT ( 'NONE',  ( -8.160000000000000142, -10.65233964170348635, -1.621096496867198589 ) ) ;
#36582=DIRECTION ( 'NONE',  ( 0.000000000000000000, -5.204170427930421283E-15, 1.000000000000000000 ) ) ;
#36599=EDGE_LOOP ( 'NONE', ( #67562, #78182, #46068, #5421 ) ) ;
#36632=VERTEX_POINT ( 'NONE', #775 ) ;
#36693=EDGE_CURVE ( 'NONE', #31601, #81299, #72797, .T. ) ;
#36717=EDGE_LOOP ( 'NONE', ( #44149, #63575 ) ) ;
#36748=CARTESIAN_POINT ( 'NONE',  ( -7.160000000000000142, -7.572993419422048511, 8.500388862211309515 ) ) ;
#36756=AXIS2_PLACEMENT_3D ( 'NONE', #20478, #29092, #43831 ) ;
#36771=FACE_OUTER_BOUND ( 'NONE', #174, .T. ) ;
#36811=DIRECTION ( 'NONE',  ( 1.000000000000000000, -0.000000000000000000, -0.000000000000000000 ) ) ;
#36832=CIRCLE ( 'NONE', #62780, 20.00000000000000000 ) ;
#36841=ORIENTED_EDGE ( 'NONE', *, *, #40849, .F. ) ;
#36887=EDGE_CURVE ( 'NONE', #95068, #33918, #32094, .T. ) ;
#36890=EDGE_CURVE ( 'NONE', #34658, #19777, #63634, .T. ) ;
#36918=DIRECTION ( 'NONE',  ( 1.000000000000000000, 0.000000000000000000, 0.000000000000000000 ) ) ;
#36929=CARTESIAN_POINT ( 'NONE',  ( -8.160000000000000142, 2.939152317953647106E-16, -2.399999999999999911 ) ) ;
#36945=DIRECTION ( 'NONE',  ( -0.000000000000000000, 0.9513357669802769978, -0.3081562241202474572 ) ) ;
#36969=ORIENTED_EDGE ( 'NONE', *, *, #68630, .F. ) ;
#36998=DIRECTION ( 'NONE',  ( 1.000000000000000000, -0.000000000000000000, 0.000000000000000000 ) ) ;
#37022=DIRECTION ( 'NONE',  ( 0.000000000000000000, 0.000000000000000000, 1.000000000000000000 ) ) ;
#37067=ORIENTED_EDGE ( 'NONE', *, *, #23925, .F. ) ;
#37167=FACE_OUTER_BOUND ( 'NONE', #99694, .T. ) ;
#37306=VECTOR ( 'NONE', #78240, 1000.000000000000000 ) ;
#37391=AXIS2_PLACEMENT_3D ( 'NONE', #1533, #63447, #24854 ) ;
#37394=LINE ( 'NONE', #68342, #4305 ) ;
#37409=DIRECTION ( 'NONE',  ( 1.000000000000000000, -0.000000000000000000, 0.000000000000000000 ) ) ;
#37429=ADVANCED_FACE ( 'NONE', ( #5910 ), #67831, .T. ) ;
#37459=VECTOR ( 'NONE', #10188, 1000.000000000000114 ) ;
#37527=SPHERICAL_SURFACE ( 'NONE', #86999, 1.000000000000000000 ) ;
#37774=DIRECTION ( 'NONE',  ( -1.000000000000000000, 0.000000000000000000, -0.000000000000000000 ) ) ;
#37848=CARTESIAN_POINT ( 'NONE',  ( 7.160000000000000142, 10.80195425911416507, -0.9450485415980990345 ) ) ;
#37870=ORIENTED_EDGE ( 'NONE', *, *, #74880, .F. ) ;
#37883=FACE_OUTER_BOUND ( 'NONE', #70910, .T. ) ;
#37992=PLANE ( 'NONE',  #15151 ) ;
#38023=DIRECTION ( 'NONE',  ( -1.000000000000000000, -0.000000000000000000, -0.000000000000000000 ) ) ;
#38037=CARTESIAN_POINT ( 'NONE',  ( -7.160000000000000142, 7.891155995661682354, 5.788828319098143993 ) ) ;
#38114=CARTESIAN_POINT ( 'NONE',  ( 8.160000000000000142, -9.074990544709798712, -0.7360493640965781736 ) ) ;
#38416=AXIS2_PLACEMENT_3D ( 'NONE', #90397, #43729, #27510 ) ;
#38486=CIRCLE ( 'NONE', #62772, 0.9999999999999997780 ) ;
#38544=ADVANCED_FACE ( 'NONE', ( #32379 ), #37992, .T. ) ;
#38553=CIRCLE ( 'NONE', #100084, 1.000000000000000000 ) ;
#38579=ORIENTED_EDGE ( 'NONE', *, *, #93870, .T. ) ;
#38627=CIRCLE ( 'NONE', #1344, 1.306876713926001354 ) ;
#38752=AXIS2_PLACEMENT_3D ( 'NONE', #17331, #25948, #2130 ) ;
#38820=AXIS2_PLACEMENT_3D ( 'NONE', #30111, #59091, #52969 ) ;
#38843=DIRECTION ( 'NONE',  ( 1.000000000000000000, 0.000000000000000000, 0.000000000000000000 ) ) ;
#38887=DIRECTION ( 'NONE',  ( -1.000000000000000000, -0.000000000000000000, -0.000000000000000000 ) ) ;
#38891=EDGE_CURVE ( 'NONE', #61060, #54056, #84819, .T. ) ;
#38938=VERTEX_POINT ( 'NONE', #78787 ) ;
#38970=DIRECTION ( 'NONE',  ( 0.000000000000000000, 3.563215788492900483E-15, -1.000000000000000000 ) ) ;
#38974=ORIENTED_EDGE ( 'NONE', *, *, #9811, .T. ) ;
#39142=DIRECTION ( 'NONE',  ( 0.000000000000000000, -1.000000000000000000, 0.000000000000000000 ) ) ;
#39153=ORIENTED_EDGE ( 'NONE', *, *, #2051, .T. ) ;
#39161=CARTESIAN_POINT ( 'NONE',  ( -6.660000000000001030, -10.15233964170348457, -1.303165529866009420 ) ) ;
#39162=CARTESIAN_POINT ( 'NONE',  ( 6.660000000000001030, 8.793627758918228565, -2.994553991265763049 ) ) ;
#39257=CARTESIAN_POINT ( 'NONE',  ( 8.160000000000000142, -5.396855673853237919E-16, 5.288828319098142217 ) ) ;
#39264=CARTESIAN_POINT ( 'NONE',  ( 6.660000000000001030, 0.000000000000000000, 0.000000000000000000 ) ) ;
#39292=ORIENTED_EDGE ( 'NONE', *, *, #78461, .T. ) ;
#39399=CARTESIAN_POINT ( 'NONE',  ( 7.160000000000000142, -6.754662360505033547, 7.925641719537454222 ) ) ;
#39464=ORIENTED_EDGE ( 'NONE', *, *, #29862, .T. ) ;
#39512=DIRECTION ( 'NONE',  ( 1.000000000000000000, -0.000000000000000000, -0.000000000000000000 ) ) ;
#39604=DIRECTION ( 'NONE',  ( 0.000000000000000000, 0.9513357669802769978, -0.3081562241202474572 ) ) ;
#39650=DIRECTION ( 'NONE',  ( 0.000000000000000000, -0.000000000000000000, -1.000000000000000000 ) ) ;
#39723=EDGE_CURVE ( 'NONE', #13349, #51586, #51746, .T. ) ;
#39761=DIRECTION ( 'NONE',  ( -1.000000000000000000, 0.000000000000000000, 0.000000000000000000 ) ) ;
#39791=CIRCLE ( 'NONE', #88417, 19.00000000000000355 ) ;
#39842=LINE ( 'NONE', #33230, #87122 ) ;
#39882=CARTESIAN_POINT ( 'NONE',  ( -7.160000000000000142, 7.891155995661682354, 6.788828319098143993 ) ) ;
#39933=AXIS2_PLACEMENT_3D ( 'NONE', #92939, #71628, #15819 ) ;
#39981=VERTEX_POINT ( 'NONE', #6439 ) ;
#40072=DIRECTION ( 'NONE',  ( 1.000000000000000000, -0.000000000000000000, -0.000000000000000000 ) ) ;
#40129=DIRECTION ( 'NONE',  ( 0.000000000000000000, -1.000000000000000000, 0.000000000000000000 ) ) ;
#40152=AXIS2_PLACEMENT_3D ( 'NONE', #4151, #21345, #81767 ) ;
#40183=VECTOR ( 'NONE', #44487, 1000.000000000000000 ) ;
#40193=CARTESIAN_POINT ( 'NONE',  ( 8.160000000000000142, 2.888964624466060727, -0.2527516539682188590 ) ) ;
#40334=CARTESIAN_POINT ( 'NONE',  ( -11.16000000000000014, -9.652339641703484574, -1.621096496867199033 ) ) ;
#40368=CARTESIAN_POINT ( 'NONE',  ( 7.160000000000000142, -5.907068460905240411E-16, 5.788828319098143105 ) ) ;
#40441=CARTESIAN_POINT ( 'NONE',  ( 8.160000000000000142, 0.000000000000000000, 0.000000000000000000 ) ) ;
#40450=VERTEX_POINT ( 'NONE', #52501 ) ;
#40492=VECTOR ( 'NONE', #42019, 1000.000000000000000 ) ;
#40513=ADVANCED_FACE ( 'NONE', ( #54999 ), #100129, .T. ) ;
#40584=VECTOR ( 'NONE', #36945, 1000.000000000000000 ) ;
#40619=FACE_OUTER_BOUND ( 'NONE', #26273, .T. ) ;
#40684=EDGE_CURVE ( 'NONE', #68689, #79343, #16922, .T. ) ;
#40842=CARTESIAN_POINT ( 'NONE',  ( 6.660000000000001030, -10.97586050609889519, -0.8902240841051127784 ) ) ;
#40849=EDGE_CURVE ( 'NONE', #87869, #22875, #20788, .T. ) ;
#40888=DIRECTION ( 'NONE',  ( 0.000000000000000000, 0.000000000000000000, -1.000000000000000000 ) ) ;
#41007=CARTESIAN_POINT ( 'NONE',  ( 8.160000000000000142, -10.65233964170348635, -1.621096496867198589 ) ) ;
#41072=CARTESIAN_POINT ( 'NONE',  ( -8.160000000000000142, -0.4583917923827245389, 5.886156785137588443 ) ) ;
#41073=EDGE_CURVE ( 'NONE', #74873, #71622, #23165, .T. ) ;
#41147=CARTESIAN_POINT ( 'NONE',  ( 7.981902603654314809, -10.32819234916652640, 1.310587897985987738 ) ) ;
#41187=CIRCLE ( 'NONE', #83255, 1.000000000000000222 ) ;
#41207=ORIENTED_EDGE ( 'NONE', *, *, #9367, .F. ) ;
#41286=CARTESIAN_POINT ( 'NONE',  ( 8.160000000000000142, -10.15233964170348457, 0.003711184059992174607 ) ) ;
#41356=LINE ( 'NONE', #72310, #90277 ) ;
#41427=ORIENTED_EDGE ( 'NONE', *, *, #82307, .T. ) ;
#41508=DIRECTION ( 'NONE',  ( -1.000000000000000000, 0.000000000000000000, -0.000000000000000000 ) ) ;
#41564=CARTESIAN_POINT ( 'NONE',  ( 8.160000000000000142, -9.652339641703484574, -1.621096496867199033 ) ) ;
#41567=EDGE_CURVE ( 'NONE', #99058, #62319, #56648, .T. ) ;
#41642=CARTESIAN_POINT ( 'NONE',  ( 7.160000000000000142, -6.754662360505033547, 7.925641719537454222 ) ) ;
#41681=PLANE ( 'NONE',  #35389 ) ;
#41694=ORIENTED_EDGE ( 'NONE', *, *, #52755, .T. ) ;
#41794=DIRECTION ( 'NONE',  ( -1.000000000000000000, 0.000000000000000000, 0.000000000000000000 ) ) ;
#41964=VERTEX_POINT ( 'NONE', #65647 ) ;
#42019=DIRECTION ( 'NONE',  ( -0.000000000000000000, -0.000000000000000000, -1.000000000000000000 ) ) ;
#42056=CARTESIAN_POINT ( 'NONE',  ( 8.160000000000000142, -9.870548898049497311, 1.288651800197855746 ) ) ;
#42072=CARTESIAN_POINT ( 'NONE',  ( -7.160000000000000142, -5.907068460905239425E-16, 5.788828319098143105 ) ) ;
#42154=PLANE ( 'NONE',  #58780 ) ;
#42167=CARTESIAN_POINT ( 'NONE',  ( -11.16000000000000014, -10.65233964170348635, 1.628518864987183790 ) ) ;
#42189=ORIENTED_EDGE ( 'NONE', *, *, #7495, .T. ) ;
#42198=CARTESIAN_POINT ( 'NONE',  ( 8.160000000000000142, -10.15233964170348457, 0.003711184059992174607 ) ) ;
#42234=DIRECTION ( 'NONE',  ( 1.000000000000000000, -0.000000000000000000, 0.000000000000000000 ) ) ;
#42241=ORIENTED_EDGE ( 'NONE', *, *, #55190, .F. ) ;
#42242=CARTESIAN_POINT ( 'NONE',  ( -8.160000000000000142, -10.15233964170348457, 0.003711184059992174607 ) ) ;
#42245=VERTEX_POINT ( 'NONE', #98261 ) ;
#42256=CARTESIAN_POINT ( 'NONE',  ( 6.660000000000001030, 0.000000000000000000, 0.000000000000000000 ) ) ;
#42294=EDGE_LOOP ( 'NONE', ( #25741, #100030, #26578, #45003 ) ) ;
#42385=ORIENTED_EDGE ( 'NONE', *, *, #41567, .F. ) ;
#42437=ORIENTED_EDGE ( 'NONE', *, *, #2896, .F. ) ;
#42480=EDGE_LOOP ( 'NONE', ( #31366, #725, #42241, #19331, #16748, #73069, #3548, #30485 ) ) ;
#42532=LINE ( 'NONE', #73964, #13539 ) ;
#42551=EDGE_CURVE ( 'NONE', #92914, #99448, #766, .T. ) ;
#42570=FACE_BOUND ( 'NONE', #67191, .T. ) ;
#42647=PLANE ( 'NONE',  #11390 ) ;
#42717=ORIENTED_EDGE ( 'NONE', *, *, #66892, .F. ) ;
#42801=CYLINDRICAL_SURFACE ( 'NONE', #30087, 1.306876713926001354 ) ;
#42836=DIRECTION ( 'NONE',  ( -0.000000000000000000, -0.9513357669802769978, 0.3081562241202474572 ) ) ;
#42985=FACE_OUTER_BOUND ( 'NONE', #25554, .T. ) ;
#43025=LINE ( 'NONE', #87190, #95950 ) ;
#43155=VECTOR ( 'NONE', #86468, 1000.000000000000000 ) ;
#43157=EDGE_CURVE ( 'NONE', #61766, #75155, #71951, .T. ) ;
#43162=EDGE_CURVE ( 'NONE', #20729, #86101, #12555, .T. ) ;
#43174=EDGE_CURVE ( 'NONE', #93973, #13349, #42532, .T. ) ;
#43192=ORIENTED_EDGE ( 'NONE', *, *, #32290, .F. ) ;
#43210=AXIS2_PLACEMENT_3D ( 'NONE', #93983, #18370, #80269 ) ;
#43263=CARTESIAN_POINT ( 'NONE',  ( -8.160000000000000142, -10.15233964170348457, 0.003711184059992174607 ) ) ;
#43330=DIRECTION ( 'NONE',  ( 0.000000000000000000, -0.9967269304714136968, -0.08084198211964954695 ) ) ;
#43346=ORIENTED_EDGE ( 'NONE', *, *, #36890, .T. ) ;
#43349=VERTEX_POINT ( 'NONE', #83049 ) ;
#43428=DIRECTION ( 'NONE',  ( 1.000000000000000000, 0.000000000000000000, 0.000000000000000000 ) ) ;
#43479=ORIENTED_EDGE ( 'NONE', *, *, #94951, .T. ) ;
#43540=EDGE_LOOP ( 'NONE', ( #34079, #47567 ) ) ;
#43541=CARTESIAN_POINT ( 'NONE',  ( 8.063330319165388005, -10.15233964170352898, 1.310587897985993955 ) ) ;
#43548=CIRCLE ( 'NONE', #24043, 20.00000000000000000 ) ;
#43553=DIRECTION ( 'NONE',  ( -0.000000000000000000, 1.000000000000000000, 1.084202172485504434E-16 ) ) ;
#43612=AXIS2_PLACEMENT_3D ( 'NONE', #35443, #43553, #83088 ) ;
#43614=CIRCLE ( 'NONE', #74389, 1.699999999999999289 ) ;
#43663=DIRECTION ( 'NONE',  ( 0.000000000000000000, 0.9967269304714136968, 0.08084198211964954695 ) ) ;
#43729=DIRECTION ( 'NONE',  ( -1.000000000000000000, 0.000000000000000000, 0.000000000000000000 ) ) ;
#43751=EDGE_LOOP ( 'NONE', ( #25747, #47310, #50112, #5227 ) ) ;
#43765=CIRCLE ( 'NONE', #59927, 1.000000000000000000 ) ;
#43789=DIRECTION ( 'NONE',  ( 0.000000000000000000, 0.000000000000000000, 1.000000000000000000 ) ) ;
#43820=DIRECTION ( 'NONE',  ( 1.000000000000000000, 0.000000000000000000, 0.000000000000000000 ) ) ;
#43831=DIRECTION ( 'NONE',  ( 0.000000000000000000, -0.8183310589170136318, 0.5747471426738539613 ) ) ;
#43919=FACE_OUTER_BOUND ( 'NONE', #70875, .T. ) ;
#43942=EDGE_LOOP ( 'NONE', ( #24558, #79510, #18753, #56880 ) ) ;
#43959=CIRCLE ( 'NONE', #97408, 1.306876713926001354 ) ;
#44149=ORIENTED_EDGE ( 'NONE', *, *, #290, .T. ) ;
#44160=CARTESIAN_POINT ( 'NONE',  ( -6.660000000000001030, -2.191226316053958875E-18, 2.701633758479787833E-17 ) ) ;
#44229=DIRECTION ( 'NONE',  ( 1.000000000000000000, -0.000000000000000000, 0.000000000000000000 ) ) ;
#44230=PRODUCT ( 'Locking Button_Varsay\X2\0131\X0\lan', 'Locking Button_Varsay\X2\0131\X0\lan', '', ( #34163 ) ) ;
#44253=DIRECTION ( 'NONE',  ( 0.000000000000000000, 0.000000000000000000, -1.000000000000000000 ) ) ;
#44427=PLANE ( 'NONE',  #97010 ) ;
#44477=PLANE ( 'NONE',  #82162 ) ;
#44487=DIRECTION ( 'NONE',  ( -1.000000000000000000, -0.000000000000000000, -0.000000000000000000 ) ) ;
#44579=EDGE_LOOP ( 'NONE', ( #6241, #62204, #26145 ) ) ;
#44650=CIRCLE ( 'NONE', #96499, 2.000000000000000000 ) ;
#44658=CARTESIAN_POINT ( 'NONE',  ( -7.160000000000000142, 8.786681894035815787, 6.233837718258663507 ) ) ;
#44723=DIRECTION ( 'NONE',  ( 0.000000000000000000, 0.000000000000000000, -1.000000000000000000 ) ) ;
#44749=CYLINDRICAL_SURFACE ( 'NONE', #89565, 0.1000000000000000472 ) ;
#44846=ORIENTED_EDGE ( 'NONE', *, *, #72565, .T. ) ;
#44873=VECTOR ( 'NONE', #86102, 999.9999999999998863 ) ;
#44886=DIRECTION ( 'NONE',  ( 0.000000000000000000, 0.000000000000000000, -1.000000000000000000 ) ) ;
#44906=LINE ( 'NONE', #14429, #47287 ) ;
#44932=ORIENTED_EDGE ( 'NONE', *, *, #34236, .T. ) ;
#44935=CARTESIAN_POINT ( 'NONE',  ( -6.660000000000001030, 0.000000000000000000, 0.000000000000000000 ) ) ;
#44941=DIRECTION ( 'NONE',  ( 1.000000000000000000, -0.000000000000000000, -0.000000000000000000 ) ) ;
#44994=LINE ( 'NONE', #12526, #40183 ) ;
#45003=ORIENTED_EDGE ( 'NONE', *, *, #86156, .F. ) ;
#45142=DIRECTION ( 'NONE',  ( 1.000000000000000000, -0.000000000000000000, -0.000000000000000000 ) ) ;
#45170=EDGE_LOOP ( 'NONE', ( #7688, #82904, #91415, #18452, #90278, #13512, #96753 ) ) ;
#45188=CARTESIAN_POINT ( 'NONE',  ( -7.160000000000000142, 0.1579206558577706254, 7.788828319098143105 ) ) ;
#45283=AXIS2_PLACEMENT_3D ( 'NONE', #12713, #53295, #13211 ) ;
#45368=VERTEX_POINT ( 'NONE', #32550 ) ;
#45387=DIRECTION ( 'NONE',  ( 1.000000000000000000, -0.000000000000000000, 0.000000000000000000 ) ) ;
#45442=DIRECTION ( 'NONE',  ( 0.000000000000000000, 0.000000000000000000, -1.000000000000000000 ) ) ;
#45450=VERTEX_POINT ( 'NONE', #61852 ) ;
#45486=FACE_OUTER_BOUND ( 'NONE', #85024, .T. ) ;
#45509=DIRECTION ( 'NONE',  ( 0.000000000000000000, 0.000000000000000000, -1.000000000000000000 ) ) ;
#45568=VERTEX_POINT ( 'NONE', #41007 ) ;
#45712=VECTOR ( 'NONE', #78160, 1000.000000000000000 ) ;
#45755=AXIS2_PLACEMENT_3D ( 'NONE', #72358, #33276, #87068 ) ;
#45761=DIRECTION ( 'NONE',  ( 0.000000000000000000, 0.9967269304714136968, 0.08084198211964954695 ) ) ;
#45850=LINE ( 'NONE', #77275, #84844 ) ;
#45859=LINE ( 'NONE', #85915, #51465 ) ;
#45942=DIRECTION ( 'NONE',  ( -5.204170427930421283E-15, 1.000000000000000000, 0.000000000000000000 ) ) ;
#45982=ORIENTED_EDGE ( 'NONE', *, *, #55190, .T. ) ;
#46008=DIRECTION ( 'NONE',  ( -1.000000000000000000, 0.000000000000000000, 0.000000000000000000 ) ) ;
#46068=ORIENTED_EDGE ( 'NONE', *, *, #31121, .T. ) ;
#46101=ORIENTED_EDGE ( 'NONE', *, *, #50633, .T. ) ;
#46103=AXIS2_PLACEMENT_3D ( 'NONE', #95325, #33418, #70492 ) ;
#46217=EDGE_CURVE ( 'NONE', #73116, #36098, #5478, .T. ) ;
#46248=B_SPLINE_CURVE_WITH_KNOTS ( 'NONE', 3,
 ( #2715, #80830, #71722, #17424, #26546, #87943, #79816, #10313 ),
 .UNSPECIFIED., .F., .F.,
 ( 4, 2, 2, 4 ),
 ( 0.000000000000000000, 0.0005804693158675770098, 0.0008707039738013634548, 0.001160938631735150117 ),
 .UNSPECIFIED. ) ;
#46259=VERTEX_POINT ( 'NONE', #57676 ) ;
#46384=AXIS2_PLACEMENT_3D ( 'NONE', #78874, #85498, #15979 ) ;
#46455=VECTOR ( 'NONE', #48800, 1000.000000000000000 ) ;
#46493=CARTESIAN_POINT ( 'NONE',  ( -11.16000000000000014, -10.15233964170348457, 0.003711184059992174607 ) ) ;
#46703=VERTEX_POINT ( 'NONE', #98075 ) ;
#46735=CIRCLE ( 'NONE', #59715, 1.699999999999999289 ) ;
#46760=CIRCLE ( 'NONE', #24069, 2.399999999999999911 ) ;
#46852=EDGE_LOOP ( 'NONE', ( #65940, #55824, #42437, #51946, #69028, #95146, #74407 ) ) ;
#46936=VERTEX_POINT ( 'NONE', #79747 ) ;
#46986=LINE ( 'NONE', #23624, #94081 ) ;
#47111=EDGE_CURVE ( 'NONE', #3020, #16367, #63046, .T. ) ;
#47144=CARTESIAN_POINT ( 'NONE',  ( 8.160000000000000142, -10.65233964170348635, 1.628518864987183790 ) ) ;
#47169=CIRCLE ( 'NONE', #1827, 2.899999999999999911 ) ;
#47287=VECTOR ( 'NONE', #6328, 1000.000000000000000 ) ;
#47310=ORIENTED_EDGE ( 'NONE', *, *, #75938, .T. ) ;
#47334=DIRECTION ( 'NONE',  ( -1.000000000000000000, 0.000000000000000000, 0.000000000000000000 ) ) ;
#47346=CYLINDRICAL_SURFACE ( 'NONE', #31755, 2.399999999999999911 ) ;
#47526=TOROIDAL_SURFACE ( 'NONE', #8699, 2.000000000000000000, 1.000000000000000000 ) ;
#47539=DIRECTION ( 'NONE',  ( 0.000000000000000000, 1.000000000000000000, 0.000000000000000000 ) ) ;
#47567=ORIENTED_EDGE ( 'NONE', *, *, #1241, .F. ) ;
#47611=ORIENTED_EDGE ( 'NONE', *, *, #33869, .T. ) ;
#47616=CARTESIAN_POINT ( 'NONE',  ( 8.160000000000000142, 1.527978830621527617, 4.717155776778118259 ) ) ;
#47706=CARTESIAN_POINT ( 'NONE',  ( -8.160000000000000142, -10.65233964170348635, -1.203735189656879756 ) ) ;
#47716=EDGE_CURVE ( 'NONE', #43349, #27461, #55574, .T. ) ;
#47734=VERTEX_POINT ( 'NONE', #2788 ) ;
#47863=LINE ( 'NONE', #78784, #85416 ) ;
#47992=AXIS2_PLACEMENT_3D ( 'NONE', #90551, #91544, #67736 ) ;
#48052=DIRECTION ( 'NONE',  ( 0.000000000000000000, 0.000000000000000000, -1.000000000000000000 ) ) ;
#48074=VERTEX_POINT ( 'NONE', #73174 ) ;
#48137=ADVANCED_FACE ( 'NONE', ( #20355 ), #65085, .T. ) ;
#48295=ORIENTED_EDGE ( 'NONE', *, *, #41073, .T. ) ;
#48451=CARTESIAN_POINT ( 'NONE',  ( 1.542438661763949392, 2.939152317953647106E-16, -2.399999999999999911 ) ) ;
#48535=CARTESIAN_POINT ( 'NONE',  ( 8.160000000000000142, -7.572993419422045847, 8.500388862211309515 ) ) ;
#48551=CIRCLE ( 'NONE', #55053, 0.1000000000000000472 ) ;
#48587=DIRECTION ( 'NONE',  ( 1.000000000000000000, 0.000000000000000000, 0.000000000000000000 ) ) ;
#48743=DIRECTION ( 'NONE',  ( 1.000000000000000000, -0.000000000000000000, 0.000000000000000000 ) ) ;
#48763=CARTESIAN_POINT ( 'NONE',  ( 7.545203588713008003, -10.70224338845203071, 1.194977652177498628 ) ) ;
#48800=DIRECTION ( 'NONE',  ( -1.000000000000000000, 0.000000000000000000, 0.000000000000000000 ) ) ;
#48843=( GEOMETRIC_REPRESENTATION_CONTEXT ( 3 ) GLOBAL_UNCERTAINTY_ASSIGNED_CONTEXT ( ( #60147 ) ) GLOBAL_UNIT_ASSIGNED_CONTEXT ( ( #1366, #84081, #14571 ) ) REPRESENTATION_CONTEXT ( 'NONE', 'WORKASPACE' ) );
#48846=CARTESIAN_POINT ( 'NONE',  ( -8.160000000000000142, 0.000000000000000000, 0.000000000000000000 ) ) ;
#48859=ORIENTED_EDGE ( 'NONE', *, *, #73490, .F. ) ;
#48872=ADVANCED_BREP_SHAPE_REPRESENTATION ( '', ( #8332, #37391 ), #48843 ) ;
#48875=ORIENTED_EDGE ( 'NONE', *, *, #80119, .T. ) ;
#48944=ORIENTED_EDGE ( 'NONE', *, *, #3781, .F. ) ;
#48969=CARTESIAN_POINT ( 'NONE',  ( 8.160000000000000142, 9.789768006247301813, -0.8564937190954607926 ) ) ;
#49010=CARTESIAN_POINT ( 'NONE',  ( 6.660000000000001030, -10.15233964170348457, 0.003711184059992174607 ) ) ;
#49037=CIRCLE ( 'NONE', #45755, 1.000000000000000000 ) ;
#49060=EDGE_LOOP ( 'NONE', ( #86245, #11111, #31092, #32097 ) ) ;
#49072=EDGE_LOOP ( 'NONE', ( #78794, #56443 ) ) ;
#49200=ORIENTED_EDGE ( 'NONE', *, *, #3009, .F. ) ;
#49216=EDGE_CURVE ( 'NONE', #45568, #79343, #45850, .T. ) ;
#49247=CARTESIAN_POINT ( 'NONE',  ( 8.160000000000000142, -10.15233964170348457, -1.303165529866009420 ) ) ;
#49291=DIRECTION ( 'NONE',  ( 0.000000000000000000, 0.000000000000000000, 1.000000000000000000 ) ) ;
#49296=DIRECTION ( 'NONE',  ( 1.000000000000000000, -0.000000000000000000, -0.000000000000000000 ) ) ;
#49405=PLANE ( 'NONE',  #25612 ) ;
#49420=CARTESIAN_POINT ( 'NONE',  ( -8.160000000000000142, -2.191226316053958875E-18, 2.701633758479787833E-17 ) ) ;
#49557=EDGE_CURVE ( 'NONE', #99147, #56283, #41187, .T. ) ;
#49611=VECTOR ( 'NONE', #52034, 1000.000000000000000 ) ;
#49684=DIRECTION ( 'NONE',  ( 0.000000000000000000, 1.020425574104004369E-16, -1.000000000000000000 ) ) ;
#49691=ORIENTED_EDGE ( 'NONE', *, *, #92956, .T. ) ;
#49701=CARTESIAN_POINT ( 'NONE',  ( 6.660000000000001030, -6.553980293839118509, 7.335060089566987962 ) ) ;
#49708=ORIENTED_EDGE ( 'NONE', *, *, #759, .T. ) ;
#49763=DIRECTION ( 'NONE',  ( 1.000000000000000000, 0.000000000000000000, 0.000000000000000000 ) ) ;
#49887=AXIS2_PLACEMENT_3D ( 'NONE', #67972, #67465, #90294 ) ;
#49889=ORIENTED_EDGE ( 'NONE', *, *, #86230, .T. ) ;
#49943=CYLINDRICAL_SURFACE ( 'NONE', #93514, 1.699999999999999734 ) ;
#49952=VECTOR ( 'NONE', #34057, 1000.000000000000000 ) ;
#50092=EDGE_LOOP ( 'NONE', ( #48859, #30848, #31111, #12174 ) ) ;
#50110=AXIS2_PLACEMENT_3D ( 'NONE', #31782, #38887, #94172 ) ;
#50112=ORIENTED_EDGE ( 'NONE', *, *, #28502, .T. ) ;
#50141=ORIENTED_EDGE ( 'NONE', *, *, #31358, .T. ) ;
#50159=CARTESIAN_POINT ( 'NONE',  ( 8.125595504227240085, -10.01787066753315614, 1.310587897985998174 ) ) ;
#50165=ORIENTED_EDGE ( 'NONE', *, *, #5648, .F. ) ;
#50172=LINE ( 'NONE', #41564, #93317 ) ;
#50221=VERTEX_POINT ( 'NONE', #66665 ) ;
#50285=FACE_OUTER_BOUND ( 'NONE', #58341, .T. ) ;
#50334=PLANE ( 'NONE',  #84166 ) ;
#50337=ORIENTED_EDGE ( 'NONE', *, *, #73490, .T. ) ;
#50372=DIRECTION ( 'NONE',  ( -1.000000000000000000, -0.000000000000000000, -0.000000000000000000 ) ) ;
#50391=DIRECTION ( 'NONE',  ( 0.000000000000000000, 0.08084198211964954695, -0.9967269304714136968 ) ) ;
#50454=DIRECTION ( 'NONE',  ( 1.000000000000000000, 0.000000000000000000, 0.000000000000000000 ) ) ;
#50489=VERTEX_POINT ( 'NONE', #26955 ) ;
#50556=ORIENTED_EDGE ( 'NONE', *, *, #49557, .F. ) ;
#50633=EDGE_CURVE ( 'NONE', #56283, #46259, #31474, .T. ) ;
#50757=EDGE_CURVE ( 'NONE', #72523, #63848, #50983, .T. ) ;
#50786=AXIS2_PLACEMENT_3D ( 'NONE', #36416, #22670, #68865 ) ;
#50847=DIRECTION ( 'NONE',  ( 0.000000000000000000, 0.000000000000000000, -1.000000000000000000 ) ) ;
#50983=CIRCLE ( 'NONE', #62345, 1.306876713926001354 ) ;
#51038=FACE_BOUND ( 'NONE', #36717, .T. ) ;
#51114=VECTOR ( 'NONE', #56560, 1000.000000000000000 ) ;
#51155=EDGE_CURVE ( 'NONE', #53334, #80380, #70912, .T. ) ;
#51248=VECTOR ( 'NONE', #7055, 1000.000000000000000 ) ;
#51347=VERTEX_POINT ( 'NONE', #58189 ) ;
#51462=DIRECTION ( 'NONE',  ( 0.000000000000000000, 0.000000000000000000, -1.000000000000000000 ) ) ;
#51465=VECTOR ( 'NONE', #69187, 1000.000000000000000 ) ;
#51493=AXIS2_PLACEMENT_3D ( 'NONE', #89779, #90772, #66954 ) ;
#51530=CIRCLE ( 'NONE', #69336, 1.306876713926001354 ) ;
#51546=CARTESIAN_POINT ( 'NONE',  ( -6.660000000000001030, -9.123836073446797812, -2.666350264951732552 ) ) ;
#51579=ORIENTED_EDGE ( 'NONE', *, *, #36887, .F. ) ;
#51586=VERTEX_POINT ( 'NONE', #1769 ) ;
#51643=EDGE_CURVE ( 'NONE', #21243, #54056, #58558, .T. ) ;
#51711=EDGE_LOOP ( 'NONE', ( #11255, #87893, #78070, #34043, #23098, #38974 ) ) ;
#51746=LINE ( 'NONE', #36504, #99230 ) ;
#51853=ORIENTED_EDGE ( 'NONE', *, *, #98598, .F. ) ;
#51862=CIRCLE ( 'NONE', #27527, 19.00000000000000355 ) ;
#51946=ORIENTED_EDGE ( 'NONE', *, *, #21897, .F. ) ;
#52034=DIRECTION ( 'NONE',  ( -1.000000000000000000, -0.000000000000000000, -0.000000000000000000 ) ) ;
#52071=DIRECTION ( 'NONE',  ( 0.000000000000000000, 0.000000000000000000, -1.000000000000000000 ) ) ;
#52087=FACE_OUTER_BOUND ( 'NONE', #31706, .T. ) ;
#52106=DIRECTION ( 'NONE',  ( -0.000000000000000000, 0.08715574274766166307, 0.9961946980917452121 ) ) ;
#52196=VECTOR ( 'NONE', #61721, 1000.000000000000000 ) ;
#52314=ORIENTED_EDGE ( 'NONE', *, *, #32762, .T. ) ;
#52369=VECTOR ( 'NONE', #71485, 1000.000000000000000 ) ;
#52394=CARTESIAN_POINT ( 'NONE',  ( -8.160000000000000142, -9.652339641703484574, 1.628518864987183790 ) ) ;
#52427=ORIENTED_EDGE ( 'NONE', *, *, #82517, .F. ) ;
#52499=DIRECTION ( 'NONE',  ( 1.000000000000000000, 0.000000000000000000, 0.000000000000000000 ) ) ;
#52501=CARTESIAN_POINT ( 'NONE',  ( -6.660000000000001030, -2.890508098367099432, -0.2344417481469836528 ) ) ;
#52579=CARTESIAN_POINT ( 'NONE',  ( 7.423834877195115922, 10.77516967368741163, -0.9427051940160163790 ) ) ;
#52704=AXIS2_PLACEMENT_3D ( 'NONE', #14970, #45942, #60675 ) ;
#52755=EDGE_CURVE ( 'NONE', #72664, #36632, #86252, .T. ) ;
#52826=EDGE_LOOP ( 'NONE', ( #58719, #65682, #10720, #95866 ) ) ;
#52843=CIRCLE ( 'NONE', #86868, 1.306876713926001798 ) ;
#52889=CARTESIAN_POINT ( 'NONE',  ( -6.660000000000001030, -10.15233964170348457, 0.003711184059992174607 ) ) ;
#52923=EDGE_CURVE ( 'NONE', #65066, #46259, #18717, .T. ) ;
#52950=AXIS2_PLACEMENT_3D ( 'NONE', #24129, #55099, #54106 ) ;
#52969=DIRECTION ( 'NONE',  ( 0.000000000000000000, -8.673617379884035472E-16, -1.000000000000000000 ) ) ;
#52980=DIRECTION ( 'NONE',  ( 0.000000000000000000, 0.000000000000000000, -1.000000000000000000 ) ) ;
#52981=AXIS2_PLACEMENT_3D ( 'NONE', #96588, #95594, #27087 ) ;
#52984=EDGE_CURVE ( 'NONE', #54393, #68497, #83465, .T. ) ;
#53005=CARTESIAN_POINT ( 'NONE',  ( 11.16000000000000014, -10.15233964170348457, 0.003711184059992174607 ) ) ;
#53029=AXIS2_PLACEMENT_3D ( 'NONE', #5307, #68214, #44886 ) ;
#53034=ORIENTED_EDGE ( 'NONE', *, *, #61512, .F. ) ;
#53092=PLANE ( 'NONE',  #2726 ) ;
#53130=AXIS2_PLACEMENT_3D ( 'NONE', #64699, #89006, #96119 ) ;
#53260=AXIS2_PLACEMENT_3D ( 'NONE', #61497, #62493, #29525 ) ;
#53265=VERTEX_POINT ( 'NONE', #8775 ) ;
#53295=DIRECTION ( 'NONE',  ( 1.000000000000000000, 0.000000000000000000, -0.000000000000000000 ) ) ;
#53317=ORIENTED_EDGE ( 'NONE', *, *, #62519, .F. ) ;
#53334=VERTEX_POINT ( 'NONE', #27508 ) ;
#53393=DIRECTION ( 'NONE',  ( 1.000000000000000000, -0.000000000000000000, 0.000000000000000000 ) ) ;
#53452=EDGE_CURVE ( 'NONE', #53334, #31601, #89995, .T. ) ;
#53524=CARTESIAN_POINT ( 'NONE',  ( -6.660000000000001030, -10.77121780415746599, 1.154761385154455366 ) ) ;
#53594=CARTESIAN_POINT ( 'NONE',  ( 8.160000000000000142, -0.4583917923827244278, 5.886156785137588443 ) ) ;
#53605=VERTEX_POINT ( 'NONE', #57788 ) ;
#53630=EDGE_CURVE ( 'NONE', #53265, #53605, #50172, .T. ) ;
#53671=AXIS2_PLACEMENT_3D ( 'NONE', #1468, #99516, #62882 ) ;
#53741=CARTESIAN_POINT ( 'NONE',  ( 8.160000000000000142, 0.1579206558577708475, 5.788828319098143105 ) ) ;
#53791=AXIS2_PLACEMENT_3D ( 'NONE', #99731, #22116, #91632 ) ;
#53983=VECTOR ( 'NONE', #81710, 1000.000000000000000 ) ;
#54055=VECTOR ( 'NONE', #81475, 1000.000000000000000 ) ;
#54056=VERTEX_POINT ( 'NONE', #53741 ) ;
#54106=DIRECTION ( 'NONE',  ( 0.000000000000000000, 0.000000000000000000, -1.000000000000000000 ) ) ;
#54175=ORIENTED_EDGE ( 'NONE', *, *, #60074, .T. ) ;
#54206=ORIENTED_EDGE ( 'NONE', *, *, #33154, .T. ) ;
#54379=ADVANCED_FACE ( 'NONE', ( #62103 ), #23501, .F. ) ;
#54393=VERTEX_POINT ( 'NONE', #35400 ) ;
#54425=CIRCLE ( 'NONE', #91717, 1.306876713926001354 ) ;
#54446=DIRECTION ( 'NONE',  ( -1.000000000000000000, 0.000000000000000000, 0.000000000000000000 ) ) ;
#54566=EDGE_LOOP ( 'NONE', ( #58078, #22697, #93848 ) ) ;
#54578=AXIS2_PLACEMENT_3D ( 'NONE', #7891, #38843, #71305 ) ;
#54716=EDGE_CURVE ( 'NONE', #55102, #93973, #52843, .T. ) ;
#54719=EDGE_CURVE ( 'NONE', #48074, #72664, #10759, .T. ) ;
#54737=ORIENTED_EDGE ( 'NONE', *, *, #10077, .F. ) ;
#54758=ORIENTED_EDGE ( 'NONE', *, *, #19906, .F. ) ;
#54930=LINE ( 'NONE', #9238, #37306 ) ;
#54999=FACE_OUTER_BOUND ( 'NONE', #19597, .T. ) ;
#55047=ORIENTED_EDGE ( 'NONE', *, *, #7716, .T. ) ;
#55053=AXIS2_PLACEMENT_3D ( 'NONE', #63683, #72282, #34217 ) ;
#55099=DIRECTION ( 'NONE',  ( 1.000000000000000000, 0.000000000000000000, 0.000000000000000000 ) ) ;
#55102=VERTEX_POINT ( 'NONE', #34029 ) ;
#55115=CARTESIAN_POINT ( 'NONE',  ( 8.160000000000000142, -9.652339641703484574, 1.628518864987183790 ) ) ;
#55144=AXIS2_PLACEMENT_3D ( 'NONE', #10539, #52106, #5422 ) ;
#55147=VECTOR ( 'NONE', #72030, 1000.000000000000000 ) ;
#55190=EDGE_CURVE ( 'NONE', #50489, #99448, #22269, .T. ) ;
#55227=EDGE_CURVE ( 'NONE', #50221, #5350, #4241, .T. ) ;
#55277=LINE ( 'NONE', #72002, #97935 ) ;
#55352=ORIENTED_EDGE ( 'NONE', *, *, #2022, .T. ) ;
#55421=PRODUCT_DEFINITION_FORMATION_WITH_SPECIFIED_SOURCE ( 'ANY', '', #44230, .NOT_KNOWN. ) ;
#55508=ADVANCED_FACE ( 'NONE', ( #30900 ), #94354, .T. ) ;
#55521=EDGE_CURVE ( 'NONE', #5872, #31685, #43025, .T. ) ;
#55574=LINE ( 'NONE', #93605, #5332 ) ;
#55676=CARTESIAN_POINT ( 'NONE',  ( 6.660000000000001030, -10.15233964170348457, 0.003711184059992174607 ) ) ;
#55690=VERTEX_POINT ( 'NONE', #4953 ) ;
#55706=ORIENTED_EDGE ( 'NONE', *, *, #81963, .F. ) ;
#55721=DIRECTION ( 'NONE',  ( -1.000000000000000000, 0.000000000000000000, -0.000000000000000000 ) ) ;
#55729=VECTOR ( 'NONE', #11065, 1000.000000000000000 ) ;
#55739=AXIS2_PLACEMENT_3D ( 'NONE', #39257, #85938, #30652 ) ;
#55824=ORIENTED_EDGE ( 'NONE', *, *, #62022, .F. ) ;
#55877=CARTESIAN_POINT ( 'NONE',  ( 7.356505681210999015, -10.77121780415745711, 1.154761385154459585 ) ) ;
#55916=EDGE_CURVE ( 'NONE', #60171, #26914, #49037, .T. ) ;
#55993=ORIENTED_EDGE ( 'NONE', *, *, #69635, .T. ) ;
#56099=AXIS2_PLACEMENT_3D ( 'NONE', #39399, #70353, #61757 ) ;
#56105=DIRECTION ( 'NONE',  ( 0.000000000000000000, -1.020425574104004369E-16, 1.000000000000000000 ) ) ;
#56123=FACE_OUTER_BOUND ( 'NONE', #93493, .T. ) ;
#56280=CARTESIAN_POINT ( 'NONE',  ( 8.160000000000000142, -6.754662360505033547, 7.925641719537452445 ) ) ;
#56283=VERTEX_POINT ( 'NONE', #6582 ) ;
#56304=FACE_OUTER_BOUND ( 'NONE', #3824, .T. ) ;
#56317=DIRECTION ( 'NONE',  ( 0.000000000000000000, 0.000000000000000000, -1.000000000000000000 ) ) ;
#56391=TOROIDAL_SURFACE ( 'NONE', #82291, 19.00000000000000000, 1.000000000000000000 ) ;
#56425=CARTESIAN_POINT ( 'NONE',  ( -7.160000000000000142, -6.754662360505034435, 7.925641719537454222 ) ) ;
#56443=ORIENTED_EDGE ( 'NONE', *, *, #29059, .T. ) ;
#56560=DIRECTION ( 'NONE',  ( 0.000000000000000000, -0.9967269304714136968, -0.08084198211964954695 ) ) ;
#56572=DIRECTION ( 'NONE',  ( -1.000000000000000000, 0.000000000000000000, 0.000000000000000000 ) ) ;
#56648=LINE ( 'NONE', #48535, #54055 ) ;
#56803=CARTESIAN_POINT ( 'NONE',  ( 6.660000000000001030, 0.000000000000000000, 0.000000000000000000 ) ) ;
#56843=EDGE_CURVE ( 'NONE', #63848, #93973, #75960, .T. ) ;
#56880=ORIENTED_EDGE ( 'NONE', *, *, #99262, .F. ) ;
#56978=VERTEX_POINT ( 'NONE', #15565 ) ;
#57088=EDGE_CURVE ( 'NONE', #16367, #4780, #30236, .T. ) ;
#57092=CARTESIAN_POINT ( 'NONE',  ( 8.160000000000000142, -10.15233964170348457, 0.003711184059992174607 ) ) ;
#57234=ORIENTED_EDGE ( 'NONE', *, *, #98537, .F. ) ;
#57349=EDGE_LOOP ( 'NONE', ( #55706, #26221, #58404, #13370 ) ) ;
#57460=DIRECTION ( 'NONE',  ( 0.000000000000000000, 0.000000000000000000, -1.000000000000000000 ) ) ;
#57551=FACE_OUTER_BOUND ( 'NONE', #94363, .T. ) ;
#57642=AXIS2_PLACEMENT_3D ( 'NONE', #98264, #89674, #20150 ) ;
#57676=CARTESIAN_POINT ( 'NONE',  ( -7.160000000000000142, 0.1579206558577707364, 6.788828319098143105 ) ) ;
#57788=CARTESIAN_POINT ( 'NONE',  ( 8.160000000000000142, -9.652339641703484574, 1.560255187525485976 ) ) ;
#57824=ORIENTED_EDGE ( 'NONE', *, *, #28139, .T. ) ;
#57874=CARTESIAN_POINT ( 'NONE',  ( -8.160000000000000142, -10.15233964170348457, 0.003711184059992174607 ) ) ;
#57942=ORIENTED_EDGE ( 'NONE', *, *, #16225, .F. ) ;
#57944=VERTEX_POINT ( 'NONE', #59976 ) ;
#57962=CIRCLE ( 'NONE', #32005, 1.306876713926001354 ) ;
#57994=CARTESIAN_POINT ( 'NONE',  ( 8.160000000000000142, -10.98394470431085601, -0.7905513910579705650 ) ) ;
#58013=CARTESIAN_POINT ( 'NONE',  ( 8.160000000000000142, -2.191226316053958875E-18, 2.701633758479787833E-17 ) ) ;
#58023=ORIENTED_EDGE ( 'NONE', *, *, #52984, .T. ) ;
#58056=VECTOR ( 'NONE', #89957, 1000.000000000000000 ) ;
#58064=ORIENTED_EDGE ( 'NONE', *, *, #10891, .F. ) ;
#58078=ORIENTED_EDGE ( 'NONE', *, *, #27449, .F. ) ;
#58189=CARTESIAN_POINT ( 'NONE',  ( 8.160000000000000142, -10.65233964170348635, -1.203735189656879756 ) ) ;
#58238=LINE ( 'NONE', #10548, #40492 ) ;
#58296=ORIENTED_EDGE ( 'NONE', *, *, #39723, .T. ) ;
#58341=EDGE_LOOP ( 'NONE', ( #4814, #6530 ) ) ;
#58351=CARTESIAN_POINT ( 'NONE',  ( -8.160000000000000142, 0.000000000000000000, 0.000000000000000000 ) ) ;
#58404=ORIENTED_EDGE ( 'NONE', *, *, #69641, .T. ) ;
#58410=AXIS2_PLACEMENT_3D ( 'NONE', #51546, #91088, #35323 ) ;
#58420=ORIENTED_EDGE ( 'NONE', *, *, #81394, .F. ) ;
#58426=EDGE_CURVE ( 'NONE', #61060, #75155, #85176, .T. ) ;
#58486=DIRECTION ( 'NONE',  ( 1.000000000000000000, 0.000000000000000000, -0.000000000000000000 ) ) ;
#58558=LINE ( 'NONE', #96603, #23481 ) ;
#58595=CARTESIAN_POINT ( 'NONE',  ( 8.160000000000000142, -10.65233964170348635, 1.628518864987183790 ) ) ;
#58643=CARTESIAN_POINT ( 'NONE',  ( 8.160000000000000142, -10.15233964170348457, 0.003711184059992174607 ) ) ;
#58712=CARTESIAN_POINT ( 'NONE',  ( 8.160000000000000142, -10.65233964170348635, 0.003711184059992174607 ) ) ;
#58719=ORIENTED_EDGE ( 'NONE', *, *, #22151, .F. ) ;
#58760=CARTESIAN_POINT ( 'NONE',  ( 8.160000000000000142, -9.728493947732140157, 1.239948043688426926 ) ) ;
#58780=AXIS2_PLACEMENT_3D ( 'NONE', #11182, #49763, #45509 ) ;
#58790=EDGE_LOOP ( 'NONE', ( #73134, #41427, #39153, #37067, #24329 ) ) ;
#58828=AXIS2_PLACEMENT_3D ( 'NONE', #39162, #70118, #599 ) ;
#58844=EDGE_CURVE ( 'NONE', #50489, #53334, #54425, .T. ) ;
#58889=LINE ( 'NONE', #44160, #6782 ) ;
#58892=CARTESIAN_POINT ( 'NONE',  ( 11.16000000000000014, -10.15233964170348457, 0.003711184059992174607 ) ) ;
#58940=ADVANCED_FACE ( 'NONE', ( #21522 ), #76307, .T. ) ;
#58953=ORIENTED_EDGE ( 'NONE', *, *, #71330, .T. ) ;
#58982=ADVANCED_FACE ( 'NONE', ( #36771 ), #5314, .T. ) ;
#59022=CYLINDRICAL_SURFACE ( 'NONE', #78528, 1.000000000000000888 ) ;
#59056=CARTESIAN_POINT ( 'NONE',  ( -6.660000000000001030, 1.527978830621527617, 4.717155776778118259 ) ) ;
#59072=ADVANCED_FACE ( 'NONE', ( #94929 ), #87823, .F. ) ;
#59091=DIRECTION ( 'NONE',  ( -1.000000000000000000, 0.000000000000000000, -0.000000000000000000 ) ) ;
#59248=DIRECTION ( 'NONE',  ( 0.000000000000000000, 0.000000000000000000, -1.000000000000000000 ) ) ;
#59336=LINE ( 'NONE', #29877, #85908 ) ;
#59476=ORIENTED_EDGE ( 'NONE', *, *, #22151, .T. ) ;
#59603=APPLICATION_CONTEXT ( 'configuration controlled 3d designs of mechanical parts and assemblies' ) ;
#59616=EDGE_LOOP ( 'NONE', ( #51853, #43479, #4137, #87778, #63296, #57824, #90647, #79776, #73303, #92589, #4811, #99344 ) ) ;
#59639=AXIS2_PLACEMENT_3D ( 'NONE', #5321, #28169, #36284 ) ;
#59692=CARTESIAN_POINT ( 'NONE',  ( -8.159999999999998366, 9.922373532429842768, -0.8680951993573241543 ) ) ;
#59715=AXIS2_PLACEMENT_3D ( 'NONE', #61264, #94182, #86577 ) ;
#59736=VECTOR ( 'NONE', #18448, 1000.000000000000000 ) ;
#59902=DIRECTION ( 'NONE',  ( 0.000000000000000000, 0.000000000000000000, -1.000000000000000000 ) ) ;
#59927=AXIS2_PLACEMENT_3D ( 'NONE', #89320, #64013, #17810 ) ;
#59962=DIRECTION ( 'NONE',  ( 1.000000000000000000, -0.000000000000000000, -0.000000000000000000 ) ) ;
#59976=CARTESIAN_POINT ( 'NONE',  ( -6.660000000000001030, -0.2368809837866516499, 5.288828319098142217 ) ) ;
#60074=EDGE_CURVE ( 'NONE', #43349, #39981, #62622, .T. ) ;
#60147=UNCERTAINTY_MEASURE_WITH_UNIT (LENGTH_MEASURE( 1.000000000000000082E-05 ), #1366, 'distance_accuracy_value', 'NONE');
#60166=DIRECTION ( 'NONE',  ( 0.000000000000000000, 0.000000000000000000, -1.000000000000000000 ) ) ;
#60171=VERTEX_POINT ( 'NONE', #19981 ) ;
#60177=ORIENTED_EDGE ( 'NONE', *, *, #27462, .T. ) ;
#60208=DIRECTION ( 'NONE',  ( 0.000000000000000000, -0.3081562241202474572, -0.9513357669802769978 ) ) ;
#60333=EDGE_CURVE ( 'NONE', #45368, #40450, #88553, .T. ) ;
#60353=DIRECTION ( 'NONE',  ( 1.000000000000000000, -0.000000000000000000, -0.000000000000000000 ) ) ;
#60378=VECTOR ( 'NONE', #50454, 1000.000000000000000 ) ;
#60393=DIRECTION ( 'NONE',  ( 1.000000000000000000, -0.000000000000000000, -0.000000000000000000 ) ) ;
#60448=CARTESIAN_POINT ( 'NONE',  ( -7.160000000000000142, 7.891155995661686795, 5.788828319098143993 ) ) ;
#60509=FACE_OUTER_BOUND ( 'NONE', #57349, .T. ) ;
#60604=FACE_OUTER_BOUND ( 'NONE', #64184, .T. ) ;
#60668=CARTESIAN_POINT ( 'NONE',  ( -8.160000000000000142, -10.15233964170348457, 0.003711184059992174607 ) ) ;
#60675=DIRECTION ( 'NONE',  ( -1.000000000000000000, -5.204170427930421283E-15, 0.000000000000000000 ) ) ;
#60681=CARTESIAN_POINT ( 'NONE',  ( 8.063330319165388005, -10.15233964170352898, 1.310587897985993955 ) ) ;
#60717=ORIENTED_EDGE ( 'NONE', *, *, #36693, .F. ) ;
#60782=ADVANCED_FACE ( 'NONE', ( #42985 ), #34366, .T. ) ;
#60802=LINE ( 'NONE', #99820, #40584 ) ;
#60883=ADVANCED_FACE ( 'NONE', ( #83517 ), #53092, .T. ) ;
#60965=AXIS2_PLACEMENT_3D ( 'NONE', #98905, #45142, #68965 ) ;
#60998=PLANE ( 'NONE',  #87389 ) ;
#61002=EDGE_CURVE ( 'NONE', #68689, #79343, #61105, .T. ) ;
#61046=ORIENTED_EDGE ( 'NONE', *, *, #46217, .F. ) ;
#61060=VERTEX_POINT ( 'NONE', #53594 ) ;
#61064=CIRCLE ( 'NONE', #52950, 1.699999999999999289 ) ;
#61105=CIRCLE ( 'NONE', #54578, 1.699999999999999289 ) ;
#61164=CARTESIAN_POINT ( 'NONE',  ( -8.160000000000000142, -10.65233964170348635, 1.628518864987183790 ) ) ;
#61195=CARTESIAN_POINT ( 'NONE',  ( -7.686499194032762716, 10.69006800129435497, -0.9352597624345265759 ) ) ;
#61207=CARTESIAN_POINT ( 'NONE',  ( 7.961587039082260731, 10.40935432823260776, -0.9107004983449004110 ) ) ;
#61208=DIRECTION ( 'NONE',  ( 0.000000000000000000, 0.9961946980917452121, -0.08715574274766166307 ) ) ;
#61225=CARTESIAN_POINT ( 'NONE',  ( -7.160000000000000142, -6.927494035009244411E-16, 6.788828319098143105 ) ) ;
#61241=CARTESIAN_POINT ( 'NONE',  ( 8.160000000000000142, -10.15233964170348457, 0.003711184059992174607 ) ) ;
#61264=CARTESIAN_POINT ( 'NONE',  ( -8.160000000000000142, -10.15233964170348457, 0.003711184059992174607 ) ) ;
#61497=CARTESIAN_POINT ( 'NONE',  ( -7.160000000000000142, -9.123836073446797812, -2.666350264951732552 ) ) ;
#61512=EDGE_CURVE ( 'NONE', #95068, #50221, #1118, .T. ) ;
#61581=ADVANCED_FACE ( 'NONE', ( #4670 ), #12258, .T. ) ;
#61668=CIRCLE ( 'NONE', #68106, 19.00000000000000000 ) ;
#61676=ORIENTED_EDGE ( 'NONE', *, *, #22168, .F. ) ;
#61721=DIRECTION ( 'NONE',  ( 0.000000000000000000, -1.000000000000000000, -1.020425574104004246E-16 ) ) ;
#61757=DIRECTION ( 'NONE',  ( 1.000000000000000000, 0.000000000000000000, 0.000000000000000000 ) ) ;
#61766=VERTEX_POINT ( 'NONE', #89284 ) ;
#61805=CARTESIAN_POINT ( 'NONE',  ( -8.160000000000000142, -2.191226316053958875E-18, 2.701633758479787833E-17 ) ) ;
#61839=VERTEX_POINT ( 'NONE', #82661 ) ;
#61852=CARTESIAN_POINT ( 'NONE',  ( -8.160000000000000142, -8.603846352786376883, -0.6978360589526751978 ) ) ;
#61872=CARTESIAN_POINT ( 'NONE',  ( -7.160000000000000142, -6.754662360505034435, 7.925641719537454222 ) ) ;
#61895=ORIENTED_EDGE ( 'NONE', *, *, #61002, .F. ) ;
#61995=CARTESIAN_POINT ( 'NONE',  ( -11.16000000000000014, -10.15233964170348457, 0.003711184059992174607 ) ) ;
#62022=EDGE_CURVE ( 'NONE', #62319, #33918, #36832, .T. ) ;
#62103=FACE_OUTER_BOUND ( 'NONE', #86235, .T. ) ;
#62204=ORIENTED_EDGE ( 'NONE', *, *, #22218, .T. ) ;
#62283=CYLINDRICAL_SURFACE ( 'NONE', #27043, 1.306876713926001354 ) ;
#62307=VERTEX_POINT ( 'NONE', #81924 ) ;
#62319=VERTEX_POINT ( 'NONE', #36748 ) ;
#62344=CARTESIAN_POINT ( 'NONE',  ( -8.063330319165405768, -10.15233964170348457, 1.310587897985993733 ) ) ;
#62345=AXIS2_PLACEMENT_3D ( 'NONE', #79122, #40072, #56317 ) ;
#62493=DIRECTION ( 'NONE',  ( 1.000000000000000000, -0.000000000000000000, 0.000000000000000000 ) ) ;
#62499=LINE ( 'NONE', #8714, #28385 ) ;
#62519=EDGE_CURVE ( 'NONE', #70921, #61839, #45859, .T. ) ;
#62588=DIRECTION ( 'NONE',  ( 1.000000000000000000, -0.000000000000000000, 0.000000000000000000 ) ) ;
#62590=EDGE_CURVE ( 'NONE', #26321, #46936, #47863, .T. ) ;
#62603=VECTOR ( 'NONE', #13436, 1000.000000000000000 ) ;
#62622=CIRCLE ( 'NONE', #65905, 1.000000000000000000 ) ;
#62633=CARTESIAN_POINT ( 'NONE',  ( 6.660000000000001030, -9.572916487583196243, -0.7764348688322058045 ) ) ;
#62649=LINE ( 'NONE', #16446, #43155 ) ;
#62742=AXIS2_PLACEMENT_3D ( 'NONE', #71698, #33125, #26012 ) ;
#62772=AXIS2_PLACEMENT_3D ( 'NONE', #100051, #86738, #17227 ) ;
#62780=AXIS2_PLACEMENT_3D ( 'NONE', #29371, #7036, #85663 ) ;
#62860=CARTESIAN_POINT ( 'NONE',  ( -8.160000000000000142, -9.728493947732140157, 1.239948043688426926 ) ) ;
#62873=CARTESIAN_POINT ( 'NONE',  ( -8.160000000000000142, -10.15233964170348457, 0.003711184059992174607 ) ) ;
#62882=DIRECTION ( 'NONE',  ( 0.000000000000000000, 0.000000000000000000, -1.000000000000000000 ) ) ;
#62898=DIRECTION ( 'NONE',  ( 1.000000000000000000, 0.000000000000000000, 0.000000000000000000 ) ) ;
#62999=CARTESIAN_POINT ( 'NONE',  ( 8.160000000000000142, 0.1579206558577706254, 7.788828319098143105 ) ) ;
#63030=AXIS2_PLACEMENT_3D ( 'NONE', #95337, #21684, #67896 ) ;
#63046=LINE ( 'NONE', #40193, #76587 ) ;
#63047=ORIENTED_EDGE ( 'NONE', *, *, #93631, .F. ) ;
#63060=DIRECTION ( 'NONE',  ( -1.000000000000000000, 0.000000000000000000, -0.000000000000000000 ) ) ;
#63065=EDGE_LOOP ( 'NONE', ( #84312, #59476 ) ) ;
#63144=ORIENTED_EDGE ( 'NONE', *, *, #5567, .F. ) ;
#63231=ADVANCED_FACE ( 'NONE', ( #83168 ), #66979, .F. ) ;
#63296=ORIENTED_EDGE ( 'NONE', *, *, #33058, .F. ) ;
#63417=CARTESIAN_POINT ( 'NONE',  ( -7.160000000000000142, -0.4583917923827245389, 5.886156785137588443 ) ) ;
#63447=DIRECTION ( 'NONE',  ( 0.000000000000000000, 0.000000000000000000, 1.000000000000000000 ) ) ;
#63575=ORIENTED_EDGE ( 'NONE', *, *, #46217, .T. ) ;
#63590=CARTESIAN_POINT ( 'NONE',  ( 1.542438661763949392, 0.000000000000000000, 0.000000000000000000 ) ) ;
#63605=DIRECTION ( 'NONE',  ( 1.000000000000000000, -0.000000000000000000, 0.000000000000000000 ) ) ;
#63634=CIRCLE ( 'NONE', #86284, 2.399999999999999911 ) ;
#63683=CARTESIAN_POINT ( 'NONE',  ( 6.660000000000001030, -10.98394470431085601, -0.7905513910579705650 ) ) ;
#63848=VERTEX_POINT ( 'NONE', #74709 ) ;
#63931=ORIENTED_EDGE ( 'NONE', *, *, #89143, .F. ) ;
#64013=DIRECTION ( 'NONE',  ( -1.000000000000000000, -0.000000000000000000, 0.000000000000000000 ) ) ;
#64045=VERTEX_POINT ( 'NONE', #22410 ) ;
#64079=DIRECTION ( 'NONE',  ( -1.000000000000000000, 0.000000000000000000, 0.000000000000000000 ) ) ;
#64099=ORIENTED_EDGE ( 'NONE', *, *, #89394, .F. ) ;
#64114=ADVANCED_FACE ( 'NONE', ( #21911 ), #69614, .T. ) ;
#64121=EDGE_CURVE ( 'NONE', #86101, #55690, #27273, .T. ) ;
#64174=CARTESIAN_POINT ( 'NONE',  ( -6.660000000000001030, -10.15233964170348457, 0.003711184059992174607 ) ) ;
#64184=EDGE_LOOP ( 'NONE', ( #36251, #46101, #253, #34237 ) ) ;
#64237=VERTEX_POINT ( 'NONE', #15811 ) ;
#64282=FACE_OUTER_BOUND ( 'NONE', #91996, .T. ) ;
#64305=ADVANCED_FACE ( 'NONE', ( #50285 ), #41681, .T. ) ;
#64315=ORIENTED_EDGE ( 'NONE', *, *, #50633, .F. ) ;
#64333=ORIENTED_EDGE ( 'NONE', *, *, #23925, .T. ) ;
#64377=EDGE_CURVE ( 'NONE', #47734, #41964, #20304, .T. ) ;
#64389=DIRECTION ( 'NONE',  ( 0.000000000000000000, 0.000000000000000000, -1.000000000000000000 ) ) ;
#64449=EDGE_CURVE ( 'NONE', #18728, #38938, #38627, .T. ) ;
#64520=DIRECTION ( 'NONE',  ( 0.000000000000000000, 0.000000000000000000, 1.000000000000000000 ) ) ;
#64611=ORIENTED_EDGE ( 'NONE', *, *, #71796, .F. ) ;
#64699=CARTESIAN_POINT ( 'NONE',  ( -8.160000000000000142, 8.793627758918228565, -2.994553991265763049 ) ) ;
#64827=ORIENTED_EDGE ( 'NONE', *, *, #9249, .F. ) ;
#64858=CARTESIAN_POINT ( 'NONE',  ( 8.160000000000000142, -2.191226316053958875E-18, 2.701633758479787833E-17 ) ) ;
#64866=CARTESIAN_POINT ( 'NONE',  ( 11.16000000000000014, -9.652339641703484574, -1.621096496867199033 ) ) ;
#64935=ORIENTED_EDGE ( 'NONE', *, *, #10014, .F. ) ;
#65011=DIRECTION ( 'NONE',  ( 0.000000000000000000, 0.000000000000000000, -1.000000000000000000 ) ) ;
#65066=VERTEX_POINT ( 'NONE', #92198 ) ;
#65085=CYLINDRICAL_SURFACE ( 'NONE', #78246, 1.000000000000000888 ) ;
#65120=DIRECTION ( 'NONE',  ( -1.000000000000000000, 0.000000000000000000, 0.000000000000000000 ) ) ;
#65132=ADVANCED_FACE ( 'NONE', ( #66893 ), #76463, .T. ) ;
#65158=LINE ( 'NONE', #49420, #85656 ) ;
#65181=VECTOR ( 'NONE', #89663, 1000.000000000000000 ) ;
#65348=ADVANCED_FACE ( 'NONE', ( #43919, #51038 ), #44427, .T. ) ;
#65637=DIRECTION ( 'NONE',  ( 0.000000000000000000, 1.000000000000000000, -0.000000000000000000 ) ) ;
#65647=CARTESIAN_POINT ( 'NONE',  ( 6.660000000000001030, -11.08332949055823846, -0.7794760011071779626 ) ) ;
#65682=ORIENTED_EDGE ( 'NONE', *, *, #21471, .T. ) ;
#65726=ORIENTED_EDGE ( 'NONE', *, *, #58426, .T. ) ;
#65813=ORIENTED_EDGE ( 'NONE', *, *, #91636, .F. ) ;
#65905=AXIS2_PLACEMENT_3D ( 'NONE', #90000, #75752, #98092 ) ;
#65940=ORIENTED_EDGE ( 'NONE', *, *, #74432, .F. ) ;
#65946=ORIENTED_EDGE ( 'NONE', *, *, #97647, .F. ) ;
#65958=AXIS2_PLACEMENT_3D ( 'NONE', #25919, #88325, #64520 ) ;
#66076=DIRECTION ( 'NONE',  ( 0.000000000000000000, -0.8955258983741306578, -0.4450093991605194033 ) ) ;
#66384=DIRECTION ( 'NONE',  ( 0.000000000000000000, 0.000000000000000000, -1.000000000000000000 ) ) ;
#66474=AXIS2_PLACEMENT_3D ( 'NONE', #58351, #73565, #97396 ) ;
#66626=ORIENTED_EDGE ( 'NONE', *, *, #19167, .T. ) ;
#66637=EDGE_CURVE ( 'NONE', #27461, #21243, #99674, .T. ) ;
#66658=ORIENTED_EDGE ( 'NONE', *, *, #22805, .T. ) ;
#66665=CARTESIAN_POINT ( 'NONE',  ( -6.660000000000001030, -10.15233964170348457, -1.303165529866009420 ) ) ;
#66687=CARTESIAN_POINT ( 'NONE',  ( -6.660000000000001030, -2.191226316053958875E-18, 2.701633758479787833E-17 ) ) ;
#66712=CARTESIAN_POINT ( 'NONE',  ( -8.160000000000000142, 2.888964624466060727, -0.2527516539682188590 ) ) ;
#66765=LINE ( 'NONE', #90076, #62603 ) ;
#66799=CARTESIAN_POINT ( 'NONE',  ( 8.160000000000000142, 0.000000000000000000, 0.000000000000000000 ) ) ;
#66825=ORIENTED_EDGE ( 'NONE', *, *, #90390, .T. ) ;
#66831=DIRECTION ( 'NONE',  ( -1.000000000000000000, 0.000000000000000000, 0.000000000000000000 ) ) ;
#66887=ORIENTED_EDGE ( 'NONE', *, *, #53452, .F. ) ;
#66892=EDGE_CURVE ( 'NONE', #4780, #31601, #97100, .T. ) ;
#66893=FACE_OUTER_BOUND ( 'NONE', #45170, .T. ) ;
#66954=DIRECTION ( 'NONE',  ( 0.000000000000000000, 0.000000000000000000, 1.000000000000000000 ) ) ;
#66979=CYLINDRICAL_SURFACE ( 'NONE', #49887, 2.399999999999999911 ) ;
#67018=CARTESIAN_POINT ( 'NONE',  ( 8.160000000000000142, -11.08332949055823846, -0.7794760011071779626 ) ) ;
#67144=CARTESIAN_POINT ( 'NONE',  ( 8.160000000000000142, -2.191226316053958875E-18, 2.701633758479787833E-17 ) ) ;
#67190=CARTESIAN_POINT ( 'NONE',  ( 6.660000000000001030, -9.074990544709798712, -0.7360493640965781736 ) ) ;
#67191=EDGE_LOOP ( 'NONE', ( #72906, #9647 ) ) ;
#67222=DIRECTION ( 'NONE',  ( 1.000000000000000000, -0.000000000000000000, -0.000000000000000000 ) ) ;
#67286=DIRECTION ( 'NONE',  ( -1.000000000000000000, 0.000000000000000000, -0.000000000000000000 ) ) ;
#67372=CIRCLE ( 'NONE', #99710, 1.699999999999999289 ) ;
#67392=CARTESIAN_POINT ( 'NONE',  ( 8.160000000000000142, 2.888964624466060727, -0.2527516539682188590 ) ) ;
#67465=DIRECTION ( 'NONE',  ( -1.000000000000000000, 0.000000000000000000, 0.000000000000000000 ) ) ;
#67562=ORIENTED_EDGE ( 'NONE', *, *, #33869, .F. ) ;
#67586=CIRCLE ( 'NONE', #62742, 0.1000000000000000472 ) ;
#67599=DIRECTION ( 'NONE',  ( -1.000000000000000000, 0.000000000000000000, -0.000000000000000000 ) ) ;
#67653=ADVANCED_FACE ( 'NONE', ( #28932 ), #80343, .F. ) ;
#67672=EDGE_CURVE ( 'NONE', #36632, #21243, #39791, .T. ) ;
#67713=ADVANCED_FACE ( 'NONE', ( #96074 ), #42801, .T. ) ;
#67736=DIRECTION ( 'NONE',  ( 1.000000000000000000, 0.000000000000000000, 0.000000000000000000 ) ) ;
#67767=AXIS2_PLACEMENT_3D ( 'NONE', #23406, #53393, #76695 ) ;
#67831=CYLINDRICAL_SURFACE ( 'NONE', #16593, 20.00000000000000000 ) ;
#67852=FACE_OUTER_BOUND ( 'NONE', #43751, .T. ) ;
#67862=ORIENTED_EDGE ( 'NONE', *, *, #27316, .F. ) ;
#67896=DIRECTION ( 'NONE',  ( 0.000000000000000000, -0.8183310589170136318, 0.5747471426738539613 ) ) ;
#67938=CARTESIAN_POINT ( 'NONE',  ( 8.160000000000000142, -9.728493947732140157, 1.239948043688426926 ) ) ;
#67972=CARTESIAN_POINT ( 'NONE',  ( 16.36243866176394945, 0.000000000000000000, 0.000000000000000000 ) ) ;
#68026=VECTOR ( 'NONE', #82153, 1000.000000000000000 ) ;
#68106=AXIS2_PLACEMENT_3D ( 'NONE', #10680, #79683, #94908 ) ;
#68214=DIRECTION ( 'NONE',  ( 1.000000000000000000, 0.000000000000000000, 0.000000000000000000 ) ) ;
#68290=CARTESIAN_POINT ( 'NONE',  ( -8.160000000000000142, 9.789768006247301813, -0.8564937190954607926 ) ) ;
#68295=VECTOR ( 'NONE', #82076, 1000.000000000000000 ) ;
#68342=CARTESIAN_POINT ( 'NONE',  ( -6.660000000000001030, -9.074990544709798712, -0.7360493640965781736 ) ) ;
#68473=CARTESIAN_POINT ( 'NONE',  ( 6.660000000000001030, -10.77121780415746599, 1.154761385154455366 ) ) ;
#68497=VERTEX_POINT ( 'NONE', #1373 ) ;
#68588=ORIENTED_EDGE ( 'NONE', *, *, #97538, .F. ) ;
#68630=EDGE_CURVE ( 'NONE', #72664, #13329, #3875, .T. ) ;
#68652=ORIENTED_EDGE ( 'NONE', *, *, #52755, .F. ) ;
#68661=DIRECTION ( 'NONE',  ( 0.000000000000000000, -9.130123557772668088E-16, -1.000000000000000000 ) ) ;
#68689=VERTEX_POINT ( 'NONE', #26700 ) ;
#68729=CARTESIAN_POINT ( 'NONE',  ( -8.160000000000000142, 0.1579206558577706254, 7.788828319098143105 ) ) ;
#68802=CARTESIAN_POINT ( 'NONE',  ( 7.777929354962648922, 10.59658755993304524, -0.9270812835540120922 ) ) ;
#68811=FACE_OUTER_BOUND ( 'NONE', #18298, .T. ) ;
#68865=DIRECTION ( 'NONE',  ( 0.000000000000000000, 0.000000000000000000, -1.000000000000000000 ) ) ;
#68942=DIRECTION ( 'NONE',  ( 0.000000000000000000, 0.9513357669802769978, -0.3081562241202474572 ) ) ;
#68965=DIRECTION ( 'NONE',  ( 0.000000000000000000, 0.000000000000000000, -1.000000000000000000 ) ) ;
#69011=EDGE_CURVE ( 'NONE', #56283, #26914, #62649, .T. ) ;
#69013=DIRECTION ( 'NONE',  ( 0.000000000000000000, 0.000000000000000000, -1.000000000000000000 ) ) ;
#69028=ORIENTED_EDGE ( 'NONE', *, *, #21559, .F. ) ;
#69050=AXIS2_PLACEMENT_3D ( 'NONE', #92252, #55721, #38970 ) ;
#69094=DIRECTION ( 'NONE',  ( 0.000000000000000000, 0.9967269304714136968, 0.08084198211964954695 ) ) ;
#69101=AXIS2_PLACEMENT_3D ( 'NONE', #61241, #92163, #76925 ) ;
#69150=VECTOR ( 'NONE', #18372, 1000.000000000000000 ) ;
#69187=DIRECTION ( 'NONE',  ( 1.000000000000000000, -0.000000000000000000, -0.000000000000000000 ) ) ;
#69190=CIRCLE ( 'NONE', #77286, 1.306876713926001354 ) ;
#69304=DIRECTION ( 'NONE',  ( -1.000000000000000000, -0.000000000000000000, -0.000000000000000000 ) ) ;
#69336=AXIS2_PLACEMENT_3D ( 'NONE', #11256, #42234, #3657 ) ;
#69460=EDGE_CURVE ( 'NONE', #27239, #26914, #89041, .T. ) ;
#69528=ORIENTED_EDGE ( 'NONE', *, *, #55521, .F. ) ;
#69554=ORIENTED_EDGE ( 'NONE', *, *, #51155, .F. ) ;
#69590=CARTESIAN_POINT ( 'NONE',  ( 7.160000000000000142, -9.123836073446797812, -2.666350264951732552 ) ) ;
#69614=CYLINDRICAL_SURFACE ( 'NONE', #15877, 1.306876713926001798 ) ;
#69619=CIRCLE ( 'NONE', #9648, 1.699999999999999289 ) ;
#69635=EDGE_CURVE ( 'NONE', #32857, #99058, #74470, .T. ) ;
#69641=EDGE_CURVE ( 'NONE', #97595, #51586, #69619, .T. ) ;
#69814=CARTESIAN_POINT ( 'NONE',  ( -8.160000000000000142, -9.652339641703484574, -1.621096496867199033 ) ) ;
#69836=VECTOR ( 'NONE', #42836, 1000.000000000000000 ) ;
#69890=ORIENTED_EDGE ( 'NONE', *, *, #57088, .F. ) ;
#70002=AXIS2_PLACEMENT_3D ( 'NONE', #75916, #84038, #6423 ) ;
#70023=ORIENTED_EDGE ( 'NONE', *, *, #57088, .T. ) ;
#70104=FACE_OUTER_BOUND ( 'NONE', #58790, .T. ) ;
#70118=DIRECTION ( 'NONE',  ( 1.000000000000000000, -0.000000000000000000, 0.000000000000000000 ) ) ;
#70183=AXIS2_PLACEMENT_3D ( 'NONE', #61995, #77689, #21901 ) ;
#70353=DIRECTION ( 'NONE',  ( 0.000000000000000000, 1.000000000000000000, 0.000000000000000000 ) ) ;
#70492=DIRECTION ( 'NONE',  ( 0.000000000000000000, 0.000000000000000000, -1.000000000000000000 ) ) ;
#70508=FACE_OUTER_BOUND ( 'NONE', #19603, .T. ) ;
#70517=AXIS2_PLACEMENT_3D ( 'NONE', #73304, #88027, #18503 ) ;
#70556=FACE_OUTER_BOUND ( 'NONE', #43942, .T. ) ;
#70559=CYLINDRICAL_SURFACE ( 'NONE', #88475, 2.399999999999999911 ) ;
#70646=AXIS2_PLACEMENT_3D ( 'NONE', #23013, #33533, #25417 ) ;
#70804=CARTESIAN_POINT ( 'NONE',  ( 8.160000000000000142, -10.65233964170348635, -1.621096496867198589 ) ) ;
#70812=LINE ( 'NONE', #17010, #27540 ) ;
#70856=ORIENTED_EDGE ( 'NONE', *, *, #7495, .F. ) ;
#70875=EDGE_LOOP ( 'NONE', ( #92586, #80587, #1479, #22718, #89406, #30010, #95143, #26215, #65726 ) ) ;
#70910=EDGE_LOOP ( 'NONE', ( #10878, #34752, #8109 ) ) ;
#70912=LINE ( 'NONE', #891, #21753 ) ;
#70921=VERTEX_POINT ( 'NONE', #95865 ) ;
#71091=CARTESIAN_POINT ( 'NONE',  ( 8.063330319165388005, -10.15233964170352898, 1.310587897985993955 ) ) ;
#71287=DIRECTION ( 'NONE',  ( 0.000000000000000000, 0.000000000000000000, 1.000000000000000000 ) ) ;
#71305=DIRECTION ( 'NONE',  ( 0.000000000000000000, 0.000000000000000000, -1.000000000000000000 ) ) ;
#71330=EDGE_CURVE ( 'NONE', #36098, #14495, #77009, .T. ) ;
#71485=DIRECTION ( 'NONE',  ( 1.000000000000000000, -0.000000000000000000, -0.000000000000000000 ) ) ;
#71616=DIRECTION ( 'NONE',  ( 0.000000000000000000, 0.000000000000000000, 1.000000000000000000 ) ) ;
#71622=VERTEX_POINT ( 'NONE', #74898 ) ;
#71628=DIRECTION ( 'NONE',  ( -0.000000000000000000, -0.9513357669802769978, 0.3081562241202474572 ) ) ;
#71675=ORIENTED_EDGE ( 'NONE', *, *, #92956, .F. ) ;
#71698=CARTESIAN_POINT ( 'NONE',  ( -6.660000000000001030, -10.98394470431085601, -0.7905513910579705650 ) ) ;
#71722=CARTESIAN_POINT ( 'NONE',  ( -7.543271203275294212, -10.70368373228984460, 1.194479805693834162 ) ) ;
#71796=EDGE_CURVE ( 'NONE', #26914, #61766, #59336, .T. ) ;
#71910=EDGE_LOOP ( 'NONE', ( #79425, #36841, #73736, #94420, #96632, #5395 ) ) ;
#71920=LINE ( 'NONE', #24718, #78838 ) ;
#71951=CIRCLE ( 'NONE', #99440, 1.000000000000000000 ) ;
#72002=CARTESIAN_POINT ( 'NONE',  ( 6.660000000000001030, -10.15233964170348457, 1.310587897985993955 ) ) ;
#72030=DIRECTION ( 'NONE',  ( -1.000000000000000000, -0.000000000000000000, -0.000000000000000000 ) ) ;
#72055=EDGE_CURVE ( 'NONE', #61839, #62307, #34385, .T. ) ;
#72079=CYLINDRICAL_SURFACE ( 'NONE', #19347, 1.000000000000000222 ) ;
#72153=EDGE_LOOP ( 'NONE', ( #34970, #10997, #87894, #42385 ) ) ;
#72158=EDGE_LOOP ( 'NONE', ( #90537, #66825, #75588 ) ) ;
#72171=ADVANCED_FACE ( 'NONE', ( #17655 ), #80053, .F. ) ;
#72172=CARTESIAN_POINT ( 'NONE',  ( -7.160000000000000142, 7.891155995661685019, 5.788828319098143993 ) ) ;
#72282=DIRECTION ( 'NONE',  ( 1.000000000000000000, -0.000000000000000000, 0.000000000000000000 ) ) ;
#72310=CARTESIAN_POINT ( 'NONE',  ( 8.160000000000000142, -0.2368809837866518997, 5.288828319098142217 ) ) ;
#72332=VECTOR ( 'NONE', #84684, 1000.000000000000000 ) ;
#72344=ORIENTED_EDGE ( 'NONE', *, *, #43157, .F. ) ;
#72358=CARTESIAN_POINT ( 'NONE',  ( -7.160000000000000142, -6.754662360505032659, 7.925641719537454222 ) ) ;
#72463=DIRECTION ( 'NONE',  ( 0.000000000000000000, -8.856219851039486941E-15, -1.000000000000000000 ) ) ;
#72475=DIRECTION ( 'NONE',  ( 0.000000000000000000, -0.000000000000000000, -1.000000000000000000 ) ) ;
#72517=DIRECTION ( 'NONE',  ( 0.000000000000000000, 0.000000000000000000, 1.000000000000000000 ) ) ;
#72523=VERTEX_POINT ( 'NONE', #1815 ) ;
#72563=ORIENTED_EDGE ( 'NONE', *, *, #76208, .F. ) ;
#72565=EDGE_CURVE ( 'NONE', #40450, #3797, #46986, .T. ) ;
#72607=CARTESIAN_POINT ( 'NONE',  ( 11.16000000000000014, -10.65233964170348635, -1.621096496867198589 ) ) ;
#72613=CIRCLE ( 'NONE', #28854, 19.00000000000000000 ) ;
#72644=EDGE_LOOP ( 'NONE', ( #7046, #86584 ) ) ;
#72664=VERTEX_POINT ( 'NONE', #98138 ) ;
#72700=ORIENTED_EDGE ( 'NONE', *, *, #78461, .F. ) ;
#72733=CARTESIAN_POINT ( 'NONE',  ( 8.160000000000000142, -9.652339641703484574, -1.621096496867199033 ) ) ;
#72772=DIRECTION ( 'NONE',  ( 0.000000000000000000, 0.000000000000000000, 1.000000000000000000 ) ) ;
#72787=DIRECTION ( 'NONE',  ( 0.000000000000000000, -1.000000000000000000, -1.020425574104004246E-16 ) ) ;
#72797=LINE ( 'NONE', #67190, #60378 ) ;
#72906=ORIENTED_EDGE ( 'NONE', *, *, #80119, .F. ) ;
#72926=ORIENTED_EDGE ( 'NONE', *, *, #80374, .F. ) ;
#72981=CARTESIAN_POINT ( 'NONE',  ( 6.660000000000001030, 7.578413286920094194, 5.288828319098143105 ) ) ;
#73018=CARTESIAN_POINT ( 'NONE',  ( 8.160000000000000142, 8.793627758918228565, -2.994553991265763049 ) ) ;
#73069=ORIENTED_EDGE ( 'NONE', *, *, #5196, .F. ) ;
#73100=ORIENTED_EDGE ( 'NONE', *, *, #97538, .T. ) ;
#73116=VERTEX_POINT ( 'NONE', #5183 ) ;
#73118=DIRECTION ( 'NONE',  ( 0.000000000000000000, 0.000000000000000000, -1.000000000000000000 ) ) ;
#73134=ORIENTED_EDGE ( 'NONE', *, *, #34939, .T. ) ;
#73174=CARTESIAN_POINT ( 'NONE',  ( 7.160000000000000142, 8.786681894035815787, 6.233837718258663507 ) ) ;
#73242=DIRECTION ( 'NONE',  ( 0.000000000000000000, 0.000000000000000000, -1.000000000000000000 ) ) ;
#73303=ORIENTED_EDGE ( 'NONE', *, *, #55227, .T. ) ;
#73304=CARTESIAN_POINT ( 'NONE',  ( -7.160000000000000142, 0.1579206558577708475, 5.788828319098143105 ) ) ;
#73341=ORIENTED_EDGE ( 'NONE', *, *, #2051, .F. ) ;
#73490=EDGE_CURVE ( 'NONE', #26321, #87025, #79190, .T. ) ;
#73506=DIRECTION ( 'NONE',  ( 0.000000000000000000, -1.000000000000000000, -1.020425574104004246E-16 ) ) ;
#73565=DIRECTION ( 'NONE',  ( -1.000000000000000000, 0.000000000000000000, 0.000000000000000000 ) ) ;
#73577=CARTESIAN_POINT ( 'NONE',  ( 8.160000000000000142, -10.15233964170348457, 0.003711184059992174607 ) ) ;
#73676=CARTESIAN_POINT ( 'NONE',  ( -6.660000000000001030, -10.15233964170348457, 0.003711184059992174607 ) ) ;
#73707=DIRECTION ( 'NONE',  ( 0.000000000000000000, 0.000000000000000000, -1.000000000000000000 ) ) ;
#73736=ORIENTED_EDGE ( 'NONE', *, *, #22168, .T. ) ;
#73861=EDGE_CURVE ( 'NONE', #3020, #31972, #47169, .T. ) ;
#73964=CARTESIAN_POINT ( 'NONE',  ( -8.160000000000000142, -10.65233964170348635, -1.621096496867198589 ) ) ;
#74055=AXIS2_PLACEMENT_3D ( 'NONE', #64174, #2760, #2259 ) ;
#74198=CIRCLE ( 'NONE', #53130, 19.00000000000000000 ) ;
#74389=AXIS2_PLACEMENT_3D ( 'NONE', #7845, #36811, #14453 ) ;
#74407=ORIENTED_EDGE ( 'NONE', *, *, #90390, .F. ) ;
#74432=EDGE_CURVE ( 'NONE', #33918, #21622, #46248, .T. ) ;
#74470=CIRCLE ( 'NONE', #45283, 1.000000000000000000 ) ;
#74499=ORIENTED_EDGE ( 'NONE', *, *, #15401, .F. ) ;
#74501=ORIENTED_EDGE ( 'NONE', *, *, #50757, .T. ) ;
#74569=DIRECTION ( 'NONE',  ( -1.000000000000000000, 0.000000000000000000, 0.000000000000000000 ) ) ;
#74572=ORIENTED_EDGE ( 'NONE', *, *, #77606, .F. ) ;
#74609=CIRCLE ( 'NONE', #97296, 1.000000000000000000 ) ;
#74665=DIRECTION ( 'NONE',  ( -1.000000000000000000, 0.000000000000000000, 0.000000000000000000 ) ) ;
#74709=CARTESIAN_POINT ( 'NONE',  ( -8.160000000000000142, -10.65233964170348635, 1.211157557776864291 ) ) ;
#74774=AXIS2_PLACEMENT_3D ( 'NONE', #76401, #69304, #8904 ) ;
#74808=EDGE_LOOP ( 'NONE', ( #13307, #91651, #33593, #95370 ) ) ;
#74812=CARTESIAN_POINT ( 'NONE',  ( 8.160000000000000142, -10.15233964170348457, 0.003711184059992174607 ) ) ;
#74827=CARTESIAN_POINT ( 'NONE',  ( 7.160000000000000142, 8.793627758918228565, -2.994553991265763049 ) ) ;
#74851=DIRECTION ( 'NONE',  ( 1.000000000000000000, -0.000000000000000000, 0.000000000000000000 ) ) ;
#74873=VERTEX_POINT ( 'NONE', #6080 ) ;
#74880=EDGE_CURVE ( 'NONE', #74873, #72523, #89387, .T. ) ;
#74898=CARTESIAN_POINT ( 'NONE',  ( -8.160000000000000142, -9.652339641703484574, 1.560255187525485976 ) ) ;
#75008=FACE_OUTER_BOUND ( 'NONE', #32075, .T. ) ;
#75085=CARTESIAN_POINT ( 'NONE',  ( -8.160000000000000142, -10.15233964170348457, 0.003711184059992174607 ) ) ;
#75155=VERTEX_POINT ( 'NONE', #56280 ) ;
#75256=CYLINDRICAL_SURFACE ( 'NONE', #87494, 1.306876713926001354 ) ;
#75266=CARTESIAN_POINT ( 'NONE',  ( 8.160000000000000142, -9.652339641703484574, -1.621096496867199033 ) ) ;
#75400=DIRECTION ( 'NONE',  ( 0.000000000000000000, 0.000000000000000000, -1.000000000000000000 ) ) ;
#75402=DIRECTION ( 'NONE',  ( 0.000000000000000000, 0.9513357669802769978, -0.3081562241202474572 ) ) ;
#75420=AXIS2_PLACEMENT_3D ( 'NONE', #57092, #80906, #51462 ) ;
#75588=ORIENTED_EDGE ( 'NONE', *, *, #74880, .T. ) ;
#75627=CARTESIAN_POINT ( 'NONE',  ( -6.660000000000001030, -10.15233964170348457, 1.310587897985993955 ) ) ;
#75752=DIRECTION ( 'NONE',  ( -1.000000000000000000, 0.000000000000000000, -0.000000000000000000 ) ) ;
#75815=DIRECTION ( 'NONE',  ( 0.000000000000000000, 0.000000000000000000, -1.000000000000000000 ) ) ;
#75910=AXIS2_PLACEMENT_3D ( 'NONE', #58013, #50391, #45761 ) ;
#75916=CARTESIAN_POINT ( 'NONE',  ( 6.660000000000001030, 8.793627758918228565, -2.994553991265763049 ) ) ;
#75938=EDGE_CURVE ( 'NONE', #11540, #78378, #77162, .T. ) ;
#75960=LINE ( 'NONE', #90703, #88559 ) ;
#76042=CARTESIAN_POINT ( 'NONE',  ( -8.151702937934075521, -9.871032969692315362, 1.282000701945956500 ) ) ;
#76195=PLANE ( 'NONE',  #7825 ) ;
#76208=EDGE_CURVE ( 'NONE', #54393, #53605, #10146, .T. ) ;
#76236=ORIENTED_EDGE ( 'NONE', *, *, #24130, .T. ) ;
#76307=PLANE ( 'NONE',  #31758 ) ;
#76309=AXIS2_PLACEMENT_3D ( 'NONE', #11800, #26541, #73707 ) ;
#76317=DIRECTION ( 'NONE',  ( 0.000000000000000000, 0.000000000000000000, -1.000000000000000000 ) ) ;
#76393=CARTESIAN_POINT ( 'NONE',  ( 7.293136219020367683, 10.80195425911416329, -0.9450485415980990345 ) ) ;
#76401=CARTESIAN_POINT ( 'NONE',  ( 11.16000000000000014, -10.15233964170348457, 0.003711184059992174607 ) ) ;
#76442=DIRECTION ( 'NONE',  ( -1.000000000000000000, -0.000000000000000000, -0.000000000000000000 ) ) ;
#76463=PLANE ( 'NONE',  #28992 ) ;
#76536=CARTESIAN_POINT ( 'NONE',  ( -8.160000000000001918, -9.799686150098729343, 1.264356398917767743 ) ) ;
#76582=DIRECTION ( 'NONE',  ( 1.000000000000000000, -0.000000000000000000, -0.000000000000000000 ) ) ;
#76587=VECTOR ( 'NONE', #1639, 1000.000000000000000 ) ;
#76663=DIRECTION ( 'NONE',  ( -0.000000000000000000, -0.9513357669802769978, 0.3081562241202474572 ) ) ;
#76695=DIRECTION ( 'NONE',  ( 0.000000000000000000, 0.000000000000000000, -1.000000000000000000 ) ) ;
#76767=ORIENTED_EDGE ( 'NONE', *, *, #29059, .F. ) ;
#76784=VERTEX_POINT ( 'NONE', #11306 ) ;
#76918=CARTESIAN_POINT ( 'NONE',  ( 8.160000000000000142, 8.793627758918228565, -2.994553991265763049 ) ) ;
#76925=DIRECTION ( 'NONE',  ( 0.000000000000000000, 0.000000000000000000, -1.000000000000000000 ) ) ;
#77009=LINE ( 'NONE', #1917, #35727 ) ;
#77070=CARTESIAN_POINT ( 'NONE',  ( -8.160000000000000142, -9.652339641703484574, -1.621096496867199033 ) ) ;
#77084=CIRCLE ( 'NONE', #69050, 18.50000000000000355 ) ;
#77101=DIRECTION ( 'NONE',  ( 0.000000000000000000, 1.000000000000000000, -0.000000000000000000 ) ) ;
#77145=EDGE_LOOP ( 'NONE', ( #39292, #95126, #80924 ) ) ;
#77155=CARTESIAN_POINT ( 'NONE',  ( 16.36243866176394945, 0.000000000000000000, 0.000000000000000000 ) ) ;
#77162=LINE ( 'NONE', #7665, #45712 ) ;
#77250=ORIENTED_EDGE ( 'NONE', *, *, #3009, .T. ) ;
#77273=EDGE_CURVE ( 'NONE', #46259, #43349, #86692, .T. ) ;
#77275=CARTESIAN_POINT ( 'NONE',  ( 8.160000000000000142, -10.65233964170348635, -1.621096496867198589 ) ) ;
#77286=AXIS2_PLACEMENT_3D ( 'NONE', #60668, #44941, #45442 ) ;
#77447=AXIS2_PLACEMENT_3D ( 'NONE', #39264, #39761, #23523 ) ;
#77580=LINE ( 'NONE', #92316, #20159 ) ;
#77606=EDGE_CURVE ( 'NONE', #53605, #7384, #36147, .T. ) ;
#77616=ORIENTED_EDGE ( 'NONE', *, *, #74432, .T. ) ;
#77682=ORIENTED_EDGE ( 'NONE', *, *, #30278, .T. ) ;
#77689=DIRECTION ( 'NONE',  ( 1.000000000000000000, -0.000000000000000000, -0.000000000000000000 ) ) ;
#77837=ORIENTED_EDGE ( 'NONE', *, *, #67672, .F. ) ;
#77851=CIRCLE ( 'NONE', #87593, 1.699999999999999289 ) ;
#77857=EDGE_LOOP ( 'NONE', ( #25563, #97138, #52314, #95099 ) ) ;
#77872=ADVANCED_FACE ( 'NONE', ( #60509 ), #7188, .T. ) ;
#77923=DIRECTION ( 'NONE',  ( 0.000000000000000000, 0.9961946980917452121, -0.08715574274766166307 ) ) ;
#77952=ORIENTED_EDGE ( 'NONE', *, *, #77273, .F. ) ;
#78070=ORIENTED_EDGE ( 'NONE', *, *, #9170, .F. ) ;
#78077=ORIENTED_EDGE ( 'NONE', *, *, #40849, .T. ) ;
#78160=DIRECTION ( 'NONE',  ( -0.000000000000000000, -0.000000000000000000, -1.000000000000000000 ) ) ;
#78182=ORIENTED_EDGE ( 'NONE', *, *, #5567, .T. ) ;
#78202=ADVANCED_FACE ( 'NONE', ( #82210 ), #47526, .T. ) ;
#78240=DIRECTION ( 'NONE',  ( 0.000000000000000000, 0.000000000000000000, 1.000000000000000000 ) ) ;
#78246=AXIS2_PLACEMENT_3D ( 'NONE', #18872, #4158, #26498 ) ;
#78289=CARTESIAN_POINT ( 'NONE',  ( -7.160000000000000142, 0.1579206558577706254, 7.788828319098143105 ) ) ;
#78378=VERTEX_POINT ( 'NONE', #2483 ) ;
#78414=LINE ( 'NONE', #69814, #88805 ) ;
#78461=EDGE_CURVE ( 'NONE', #7384, #92914, #10443, .T. ) ;
#78528=AXIS2_PLACEMENT_3D ( 'NONE', #89954, #82339, #43789 ) ;
#78669=CARTESIAN_POINT ( 'NONE',  ( 7.160000000000000142, -10.77121780415746599, 1.154761385154455366 ) ) ;
#78713=ADVANCED_FACE ( 'NONE', ( #6966, #82592 ), #84083, .F. ) ;
#78784=CARTESIAN_POINT ( 'NONE',  ( -6.660000000000001030, -10.97586050609889163, -0.8902240841051124454 ) ) ;
#78787=CARTESIAN_POINT ( 'NONE',  ( -8.160000000000000142, -9.074990544709798712, -0.7360493640965781736 ) ) ;
#78794=ORIENTED_EDGE ( 'NONE', *, *, #72055, .F. ) ;
#78838=VECTOR ( 'NONE', #1405, 1000.000000000000000 ) ;
#78874=CARTESIAN_POINT ( 'NONE',  ( 16.36243866176394945, 0.000000000000000000, 0.000000000000000000 ) ) ;
#78943=CARTESIAN_POINT ( 'NONE',  ( 8.160000000000000142, 0.000000000000000000, 0.000000000000000000 ) ) ;
#79056=CARTESIAN_POINT ( 'NONE',  ( -7.160000000000000142, -10.77121780415746599, 1.154761385154455366 ) ) ;
#79090=CARTESIAN_POINT ( 'NONE',  ( -7.160000000000000142, 10.80195425911416507, -0.9450485415980990345 ) ) ;
#79122=CARTESIAN_POINT ( 'NONE',  ( -8.160000000000000142, -10.15233964170348457, 0.003711184059992174607 ) ) ;
#79190=LINE ( 'NONE', #9686, #37459 ) ;
#79326=DIRECTION ( 'NONE',  ( 0.000000000000000000, 0.000000000000000000, 1.000000000000000000 ) ) ;
#79343=VERTEX_POINT ( 'NONE', #3928 ) ;
#79361=CYLINDRICAL_SURFACE ( 'NONE', #74055, 1.306876713926001798 ) ;
#79400=CARTESIAN_POINT ( 'NONE',  ( 8.159999999999996589, 9.922339117699207733, -0.8680921884585347525 ) ) ;
#79416=FACE_OUTER_BOUND ( 'NONE', #32765, .T. ) ;
#79425=ORIENTED_EDGE ( 'NONE', *, *, #5346, .F. ) ;
#79462=VECTOR ( 'NONE', #2947, 1000.000000000000000 ) ;
#79510=ORIENTED_EDGE ( 'NONE', *, *, #58426, .F. ) ;
#79600=EDGE_LOOP ( 'NONE', ( #808, #25213, #58064, #86753, #63144, #97281 ) ) ;
#79683=DIRECTION ( 'NONE',  ( 1.000000000000000000, -0.000000000000000000, 0.000000000000000000 ) ) ;
#79722=VECTOR ( 'NONE', #81222, 1000.000000000000000 ) ;
#79747=CARTESIAN_POINT ( 'NONE',  ( -6.660000000000001030, -10.97586050609889519, -0.8902240841051127784 ) ) ;
#79771=DIRECTION ( 'NONE',  ( 0.000000000000000000, 0.000000000000000000, 1.000000000000000000 ) ) ;
#79776=ORIENTED_EDGE ( 'NONE', *, *, #61512, .T. ) ;
#79789=ORIENTED_EDGE ( 'NONE', *, *, #20118, .T. ) ;
#79810=FACE_OUTER_BOUND ( 'NONE', #32869, .T. ) ;
#79816=CARTESIAN_POINT ( 'NONE',  ( -8.022773894012710016, -10.23992600125390418, 1.310587897985993511 ) ) ;
#79895=AXIS2_PLACEMENT_3D ( 'NONE', #34916, #97313, #66384 ) ;
#79918=CYLINDRICAL_SURFACE ( 'NONE', #28681, 1.000000000000000000 ) ;
#79942=DIRECTION ( 'NONE',  ( 0.000000000000000000, 0.000000000000000000, -1.000000000000000000 ) ) ;
#80044=FACE_OUTER_BOUND ( 'NONE', #1308, .T. ) ;
#80053=PLANE ( 'NONE',  #55144 ) ;
#80063=CARTESIAN_POINT ( 'NONE',  ( -8.160000000000000142, -9.123836073446797812, -2.666350264951732552 ) ) ;
#80119=EDGE_CURVE ( 'NONE', #14495, #82155, #16168, .T. ) ;
#80208=CYLINDRICAL_SURFACE ( 'NONE', #65958, 1.000000000000000000 ) ;
#80241=ADVANCED_FACE ( 'NONE', ( #70556 ), #72079, .T. ) ;
#80245=ADVANCED_FACE ( 'NONE', ( #40619 ), #35588, .T. ) ;
#80269=DIRECTION ( 'NONE',  ( 0.000000000000000000, 0.000000000000000000, -1.000000000000000000 ) ) ;
#80300=EDGE_LOOP ( 'NONE', ( #71675, #18996, #96139, #83389 ) ) ;
#80343=PLANE ( 'NONE',  #20377 ) ;
#80374=EDGE_CURVE ( 'NONE', #26606, #3797, #9724, .T. ) ;
#80380=VERTEX_POINT ( 'NONE', #49247 ) ;
#80587=ORIENTED_EDGE ( 'NONE', *, *, #27462, .F. ) ;
#80613=DIRECTION ( 'NONE',  ( 1.000000000000000000, -0.000000000000000000, 0.000000000000000000 ) ) ;
#80819=ADVANCED_FACE ( 'NONE', ( #60604 ), #29206, .T. ) ;
#80830=CARTESIAN_POINT ( 'NONE',  ( -7.357004447969931249, -10.77121780415746954, 1.154761385154455144 ) ) ;
#80873=DIRECTION ( 'NONE',  ( -1.000000000000000000, -0.000000000000000000, -0.000000000000000000 ) ) ;
#80880=CARTESIAN_POINT ( 'NONE',  ( 6.660000000000001030, -2.191226316053958875E-18, 2.701633758479787833E-17 ) ) ;
#80906=DIRECTION ( 'NONE',  ( 1.000000000000000000, 0.000000000000000000, 0.000000000000000000 ) ) ;
#80924=ORIENTED_EDGE ( 'NONE', *, *, #30525, .F. ) ;
#80949=DIRECTION ( 'NONE',  ( 1.000000000000000000, -0.000000000000000000, 0.000000000000000000 ) ) ;
#81143=AXIS2_PLACEMENT_3D ( 'NONE', #56425, #24942, #16835 ) ;
#81188=DIRECTION ( 'NONE',  ( 0.000000000000000000, 0.000000000000000000, -1.000000000000000000 ) ) ;
#81222=DIRECTION ( 'NONE',  ( 1.000000000000000000, 0.000000000000000000, 0.000000000000000000 ) ) ;
#81299=VERTEX_POINT ( 'NONE', #38114 ) ;
#81319=PLANE ( 'NONE',  #76309 ) ;
#81394=EDGE_CURVE ( 'NONE', #75155, #32857, #74609, .T. ) ;
#81428=EDGE_CURVE ( 'NONE', #75155, #54393, #61668, .T. ) ;
#81461=AXIS2_PLACEMENT_3D ( 'NONE', #82302, #58486, #44253 ) ;
#81475=DIRECTION ( 'NONE',  ( -1.000000000000000000, -0.000000000000000000, -0.000000000000000000 ) ) ;
#81536=EDGE_LOOP ( 'NONE', ( #6583, #66626, #6794, #9828, #28976 ) ) ;
#81574=ADVANCED_FACE ( 'NONE', ( #19772 ), #42647, .F. ) ;
#81710=DIRECTION ( 'NONE',  ( -0.000000000000000000, -0.000000000000000000, -1.000000000000000000 ) ) ;
#81757=ORIENTED_EDGE ( 'NONE', *, *, #71330, .F. ) ;
#81767=DIRECTION ( 'NONE',  ( 0.000000000000000000, 0.000000000000000000, -1.000000000000000000 ) ) ;
#81924=CARTESIAN_POINT ( 'NONE',  ( 11.16000000000000014, -9.652339641703484574, 1.628518864987183790 ) ) ;
#81963=EDGE_CURVE ( 'NONE', #98627, #13349, #77851, .T. ) ;
#81980=DIRECTION ( 'NONE',  ( 0.000000000000000000, 0.000000000000000000, -1.000000000000000000 ) ) ;
#82006=ORIENTED_EDGE ( 'NONE', *, *, #16327, .F. ) ;
#82011=EDGE_LOOP ( 'NONE', ( #73100, #31862, #54206, #83841 ) ) ;
#82076=DIRECTION ( 'NONE',  ( -1.000000000000000000, -0.000000000000000000, -0.000000000000000000 ) ) ;
#82098=AXIS2_PLACEMENT_3D ( 'NONE', #90623, #100200, #52071 ) ;
#82135=VERTEX_POINT ( 'NONE', #35407 ) ;
#82153=DIRECTION ( 'NONE',  ( -1.000000000000000000, -0.000000000000000000, -0.000000000000000000 ) ) ;
#82155=VERTEX_POINT ( 'NONE', #97291 ) ;
#82162=AXIS2_PLACEMENT_3D ( 'NONE', #83016, #60208, #75402 ) ;
#82210=FACE_OUTER_BOUND ( 'NONE', #16466, .T. ) ;
#82230=VERTEX_POINT ( 'NONE', #29773 ) ;
#82262=DIRECTION ( 'NONE',  ( 0.000000000000000000, 1.000000000000000000, 5.204170427930421283E-15 ) ) ;
#82291=AXIS2_PLACEMENT_3D ( 'NONE', #74827, #91055, #11938 ) ;
#82302=CARTESIAN_POINT ( 'NONE',  ( 7.160000000000000142, -6.754662360505032659, 7.925641719537454222 ) ) ;
#82307=EDGE_CURVE ( 'NONE', #5350, #38938, #37394, .T. ) ;
#82317=ADVANCED_FACE ( 'NONE', ( #67852 ), #99275, .F. ) ;
#82339=DIRECTION ( 'NONE',  ( -1.000000000000000000, -0.000000000000000000, -0.000000000000000000 ) ) ;
#82373=FACE_OUTER_BOUND ( 'NONE', #23511, .T. ) ;
#82412=ORIENTED_EDGE ( 'NONE', *, *, #91149, .T. ) ;
#82473=VERTEX_POINT ( 'NONE', #39882 ) ;
#82517=EDGE_CURVE ( 'NONE', #45368, #42245, #85049, .T. ) ;
#82592=FACE_BOUND ( 'NONE', #43540, .T. ) ;
#82661=CARTESIAN_POINT ( 'NONE',  ( 11.16000000000000014, -9.652339641703484574, -1.621096496867199033 ) ) ;
#82669=PLANE ( 'NONE',  #35224 ) ;
#82746=ADVANCED_FACE ( 'NONE', ( #12919 ), #80208, .T. ) ;
#82774=CARTESIAN_POINT ( 'NONE',  ( 6.660000000000001030, -10.15233964170348457, 0.003711184059992174607 ) ) ;
#82796=FACE_OUTER_BOUND ( 'NONE', #80300, .T. ) ;
#82904=ORIENTED_EDGE ( 'NONE', *, *, #77606, .T. ) ;
#83016=CARTESIAN_POINT ( 'NONE',  ( 8.160000000000000142, 1.990213166801898970, 6.144159427248533589 ) ) ;
#83049=CARTESIAN_POINT ( 'NONE',  ( 7.160000000000000142, 0.1579206558577707364, 6.788828319098143105 ) ) ;
#83088=DIRECTION ( 'NONE',  ( 0.000000000000000000, 1.084202172485504434E-16, -1.000000000000000000 ) ) ;
#83139=AXIS2_PLACEMENT_3D ( 'NONE', #28288, #37409, #59248 ) ;
#83168=FACE_OUTER_BOUND ( 'NONE', #98967, .T. ) ;
#83207=ADVANCED_FACE ( 'NONE', ( #15684 ), #37527, .T. ) ;
#83250=LINE ( 'NONE', #75627, #32447 ) ;
#83255=AXIS2_PLACEMENT_3D ( 'NONE', #63417, #2005, #17722 ) ;
#83389=ORIENTED_EDGE ( 'NONE', *, *, #62590, .F. ) ;
#83424=CARTESIAN_POINT ( 'NONE',  ( 8.160000000000000142, -9.652339641703484574, 0.003711184059992174607 ) ) ;
#83465=CIRCLE ( 'NONE', #75420, 1.699999999999999289 ) ;
#83517=FACE_OUTER_BOUND ( 'NONE', #72644, .T. ) ;
#83633=ADVANCED_FACE ( 'NONE', ( #99389, #6047 ), #82669, .T. ) ;
#83828=DIRECTION ( 'NONE',  ( 0.000000000000000000, 0.000000000000000000, 1.000000000000000000 ) ) ;
#83841=ORIENTED_EDGE ( 'NONE', *, *, #11851, .F. ) ;
#83847=ORIENTED_EDGE ( 'NONE', *, *, #94951, .F. ) ;
#83877=LINE ( 'NONE', #75266, #85335 ) ;
#84001=CARTESIAN_POINT ( 'NONE',  ( 8.160000000000000142, 7.891155995661686795, 5.788828319098143993 ) ) ;
#84035=CARTESIAN_POINT ( 'NONE',  ( 7.160000000000000142, 7.891155995661682354, 6.788828319098143993 ) ) ;
#84038=DIRECTION ( 'NONE',  ( 1.000000000000000000, -0.000000000000000000, 0.000000000000000000 ) ) ;
#84080=ORIENTED_EDGE ( 'NONE', *, *, #43174, .F. ) ;
#84081=( NAMED_UNIT ( * ) PLANE_ANGLE_UNIT ( ) SI_UNIT ( $, .RADIAN. ) );
#84083=PLANE ( 'NONE',  #50786 ) ;
#84152=ORIENTED_EDGE ( 'NONE', *, *, #66637, .F. ) ;
#84166=AXIS2_PLACEMENT_3D ( 'NONE', #42242, #64079, #57460 ) ;
#84178=ORIENTED_EDGE ( 'NONE', *, *, #20118, .F. ) ;
#84235=VECTOR ( 'NONE', #84827, 1000.000000000000000 ) ;
#84312=ORIENTED_EDGE ( 'NONE', *, *, #98537, .T. ) ;
#84313=DIRECTION ( 'NONE',  ( 1.000000000000000000, -0.000000000000000000, -0.000000000000000000 ) ) ;
#84426=DIRECTION ( 'NONE',  ( 0.000000000000000000, 0.000000000000000000, -1.000000000000000000 ) ) ;
#84606=CARTESIAN_POINT ( 'NONE',  ( -11.16000000000000014, -9.652339641703484574, -1.621096496867199033 ) ) ;
#84665=EDGE_LOOP ( 'NONE', ( #29415, #98831, #50556, #57942 ) ) ;
#84684=DIRECTION ( 'NONE',  ( 1.000000000000000000, 0.000000000000000000, 0.000000000000000000 ) ) ;
#84819=CIRCLE ( 'NONE', #23254, 2.000000000000000000 ) ;
#84827=DIRECTION ( 'NONE',  ( -0.000000000000000000, 1.000000000000000000, 1.020425574104004246E-16 ) ) ;
#84844=VECTOR ( 'NONE', #29615, 1000.000000000000000 ) ;
#84913=ORIENTED_EDGE ( 'NONE', *, *, #43162, .F. ) ;
#84921=EDGE_CURVE ( 'NONE', #73116, #82155, #7562, .T. ) ;
#85024=EDGE_LOOP ( 'NONE', ( #61895, #89219, #26709, #35133 ) ) ;
#85049=LINE ( 'NONE', #1833, #93434 ) ;
#85129=AXIS2_PLACEMENT_3D ( 'NONE', #1505, #77101, #86724 ) ;
#85176=LINE ( 'NONE', #15664, #51248 ) ;
#85277=AXIS2_PLACEMENT_3D ( 'NONE', #69590, #67599, #98518 ) ;
#85335=VECTOR ( 'NONE', #20974, 1000.000000000000000 ) ;
#85336=ORIENTED_EDGE ( 'NONE', *, *, #32290, .T. ) ;
#85416=VECTOR ( 'NONE', #34638, 1000.000000000000000 ) ;
#85461=EDGE_LOOP ( 'NONE', ( #89863, #57234, #55352, #43346 ) ) ;
#85498=DIRECTION ( 'NONE',  ( -1.000000000000000000, 0.000000000000000000, 0.000000000000000000 ) ) ;
#85598=LINE ( 'NONE', #40441, #44873 ) ;
#85616=ORIENTED_EDGE ( 'NONE', *, *, #69641, .F. ) ;
#85617=ADVANCED_FACE ( 'NONE', ( #4831 ), #56391, .T. ) ;
#85647=EDGE_CURVE ( 'NONE', #22875, #29959, #30430, .T. ) ;
#85656=VECTOR ( 'NONE', #12320, 1000.000000000000000 ) ;
#85663=DIRECTION ( 'NONE',  ( 0.000000000000000000, 0.000000000000000000, -1.000000000000000000 ) ) ;
#85728=CARTESIAN_POINT ( 'NONE',  ( 6.660000000000001030, 0.000000000000000000, 2.399999999999999911 ) ) ;
#85739=EDGE_LOOP ( 'NONE', ( #61046, #23441, #49708, #81757 ) ) ;
#85908=VECTOR ( 'NONE', #60353, 1000.000000000000000 ) ;
#85915=CARTESIAN_POINT ( 'NONE',  ( 8.160000000000000142, -9.652339641703484574, -1.621096496867199033 ) ) ;
#85938=DIRECTION ( 'NONE',  ( 0.000000000000000000, 1.020425574104004246E-16, -1.000000000000000000 ) ) ;
#86066=CYLINDRICAL_SURFACE ( 'NONE', #50110, 20.00000000000000355 ) ;
#86101=VERTEX_POINT ( 'NONE', #11322 ) ;
#86102=DIRECTION ( 'NONE',  ( 0.000000000000000000, 0.9961946980917453232, -0.08715574274766167695 ) ) ;
#86121=ADVANCED_FACE ( 'NONE', ( #34663 ), #27047, .T. ) ;
#86156=EDGE_CURVE ( 'NONE', #13329, #1499, #12682, .T. ) ;
#86230=EDGE_CURVE ( 'NONE', #95068, #47734, #43548, .T. ) ;
#86235=EDGE_LOOP ( 'NONE', ( #61676, #21965, #73341, #15613 ) ) ;
#86245=ORIENTED_EDGE ( 'NONE', *, *, #99840, .F. ) ;
#86252=B_SPLINE_CURVE_WITH_KNOTS ( 'NONE', 3,
 ( #37848, #76393, #52579, #6895, #68802, #61207, #7385, #23601, #79400, #48969 ),
 .UNSPECIFIED., .F., .F.,
 ( 4, 2, 2, 2, 4 ),
 ( 0.000000000000000000, 0.0003937058646109520060, 0.0007874117292219040120, 0.001181117593832857644, 0.001574823458443811493 ),
 .UNSPECIFIED. ) ;
#86273=ORIENTED_EDGE ( 'NONE', *, *, #24907, .T. ) ;
#86283=FACE_OUTER_BOUND ( 'NONE', #85739, .T. ) ;
#86284=AXIS2_PLACEMENT_3D ( 'NONE', #48846, #47334, #79771 ) ;
#86299=ADVANCED_FACE ( 'NONE', ( #14297 ), #76195, .T. ) ;
#86431=FACE_OUTER_BOUND ( 'NONE', #42294, .T. ) ;
#86468=DIRECTION ( 'NONE',  ( 0.000000000000000000, -0.9513357669802769978, 0.3081562241202474572 ) ) ;
#86577=DIRECTION ( 'NONE',  ( 0.000000000000000000, 0.000000000000000000, -1.000000000000000000 ) ) ;
#86584=ORIENTED_EDGE ( 'NONE', *, *, #5346, .T. ) ;
#86630=CARTESIAN_POINT ( 'NONE',  ( -6.660000000000001030, -10.15233964170348457, 0.003711184059992174607 ) ) ;
#86675=EDGE_CURVE ( 'NONE', #87869, #45450, #46735, .T. ) ;
#86692=LINE ( 'NONE', #92796, #52369 ) ;
#86724=DIRECTION ( 'NONE',  ( 0.000000000000000000, 0.000000000000000000, 1.000000000000000000 ) ) ;
#86738=DIRECTION ( 'NONE',  ( 0.000000000000000000, -0.4450093991605204025, 0.8955258983741301027 ) ) ;
#86753=ORIENTED_EDGE ( 'NONE', *, *, #53630, .F. ) ;
#86868=AXIS2_PLACEMENT_3D ( 'NONE', #43263, #65120, #11303 ) ;
#86898=FACE_OUTER_BOUND ( 'NONE', #52826, .T. ) ;
#86975=CARTESIAN_POINT ( 'NONE',  ( 11.16000000000000014, -10.15233964170348457, 0.003711184059992174607 ) ) ;
#86999=AXIS2_PLACEMENT_3D ( 'NONE', #21779, #6072, #91310 ) ;
#87011=ORIENTED_EDGE ( 'NONE', *, *, #80374, .T. ) ;
#87025=VERTEX_POINT ( 'NONE', #62633 ) ;
#87068=DIRECTION ( 'NONE',  ( 0.000000000000000000, -0.3081562241202470687, -0.9513357669802772199 ) ) ;
#87122=VECTOR ( 'NONE', #9891, 1000.000000000000114 ) ;
#87158=CIRCLE ( 'NONE', #40152, 2.399999999999999911 ) ;
#87190=CARTESIAN_POINT ( 'NONE',  ( 6.660000000000001030, -5.396855673853237919E-16, 5.288828319098142217 ) ) ;
#87368=ORIENTED_EDGE ( 'NONE', *, *, #5143, .T. ) ;
#87389=AXIS2_PLACEMENT_3D ( 'NONE', #586, #23919, #69094 ) ;
#87401=DIRECTION ( 'NONE',  ( 0.000000000000000000, 0.000000000000000000, 1.000000000000000000 ) ) ;
#87415=CARTESIAN_POINT ( 'NONE',  ( 8.160000000000000142, 0.1579206558577706254, 7.788828319098143105 ) ) ;
#87494=AXIS2_PLACEMENT_3D ( 'NONE', #18975, #43820, #96598 ) ;
#87577=ADVANCED_FACE ( 'NONE', ( #75008 ), #92729, .T. ) ;
#87586=AXIS2_PLACEMENT_3D ( 'NONE', #44935, #27706, #60166 ) ;
#87593=AXIS2_PLACEMENT_3D ( 'NONE', #62873, #39512, #93789 ) ;
#87597=CARTESIAN_POINT ( 'NONE',  ( -7.160000000000000142, -6.754662360505033547, 7.925641719537454222 ) ) ;
#87735=PLANE ( 'NONE',  #18636 ) ;
#87778=ORIENTED_EDGE ( 'NONE', *, *, #64121, .T. ) ;
#87791=CARTESIAN_POINT ( 'NONE',  ( 7.160000000000000142, 1.682056942681651179, 5.192823660268256702 ) ) ;
#87799=AXIS2_PLACEMENT_3D ( 'NONE', #75085, #60393, #21785 ) ;
#87823=PLANE ( 'NONE',  #70646 ) ;
#87869=VERTEX_POINT ( 'NONE', #21595 ) ;
#87893=ORIENTED_EDGE ( 'NONE', *, *, #49216, .F. ) ;
#87894=ORIENTED_EDGE ( 'NONE', *, *, #29862, .F. ) ;
#87928=VERTEX_POINT ( 'NONE', #99708 ) ;
#87943=CARTESIAN_POINT ( 'NONE',  ( -7.970484365542752414, -10.32263987662778248, 1.301654676760341856 ) ) ;
#87947=SHAPE_DEFINITION_REPRESENTATION ( #89572, #22430 ) ;
#88027=DIRECTION ( 'NONE',  ( 0.000000000000000000, 1.000000000000000000, 1.084202172485504311E-16 ) ) ;
#88028=FACE_OUTER_BOUND ( 'NONE', #51711, .T. ) ;
#88159=ORIENTED_EDGE ( 'NONE', *, *, #50757, .F. ) ;
#88238=CYLINDRICAL_SURFACE ( 'NONE', #23538, 18.50000000000000000 ) ;
#88325=DIRECTION ( 'NONE',  ( -1.000000000000000000, -0.000000000000000000, -0.000000000000000000 ) ) ;
#88417=AXIS2_PLACEMENT_3D ( 'NONE', #88464, #18939, #34677 ) ;
#88464=CARTESIAN_POINT ( 'NONE',  ( 8.160000000000000142, -9.123836073446797812, -2.666350264951732552 ) ) ;
#88475=AXIS2_PLACEMENT_3D ( 'NONE', #77155, #93384, #30991 ) ;
#88490=FACE_OUTER_BOUND ( 'NONE', #72158, .T. ) ;
#88553=CIRCLE ( 'NONE', #43210, 2.899999999999999911 ) ;
#88559=VECTOR ( 'NONE', #91686, 1000.000000000000000 ) ;
#88561=ADVANCED_FACE ( 'NONE', ( #9759 ), #50334, .F. ) ;
#88627=ORIENTED_EDGE ( 'NONE', *, *, #55521, .T. ) ;
#88669=DIRECTION ( 'NONE',  ( 0.000000000000000000, 0.9967269304714136968, 0.08084198211964954695 ) ) ;
#88696=CARTESIAN_POINT ( 'NONE',  ( 6.660000000000001030, -6.553980293839118509, 7.335060089566987962 ) ) ;
#88700=LINE ( 'NONE', #72981, #68295 ) ;
#88720=EDGE_LOOP ( 'NONE', ( #64315, #43192, #32243, #77952 ) ) ;
#88782=LINE ( 'NONE', #19248, #68026 ) ;
#88805=VECTOR ( 'NONE', #31750, 1000.000000000000000 ) ;
#88807=DIRECTION ( 'NONE',  ( 1.000000000000000000, -0.000000000000000000, 0.000000000000000000 ) ) ;
#88862=ORIENTED_EDGE ( 'NONE', *, *, #20552, .T. ) ;
#89006=DIRECTION ( 'NONE',  ( -1.000000000000000000, 0.000000000000000000, -0.000000000000000000 ) ) ;
#89041=CIRCLE ( 'NONE', #81143, 1.000000000000000888 ) ;
#89143=EDGE_CURVE ( 'NONE', #64045, #42245, #88782, .T. ) ;
#89195=CARTESIAN_POINT ( 'NONE',  ( -7.160000000000000142, 8.793627758918228565, -2.994553991265763049 ) ) ;
#89219=ORIENTED_EDGE ( 'NONE', *, *, #9811, .F. ) ;
#89230=DIRECTION ( 'NONE',  ( -1.000000000000000000, -0.000000000000000000, -0.000000000000000000 ) ) ;
#89284=CARTESIAN_POINT ( 'NONE',  ( 7.160000000000000142, -6.446506136384785535, 8.876977486517731109 ) ) ;
#89320=CARTESIAN_POINT ( 'NONE',  ( 7.160000000000000142, 7.891155995661685019, 5.788828319098143993 ) ) ;
#89387=CIRCLE ( 'NONE', #87799, 1.306876713926001354 ) ;
#89394=EDGE_CURVE ( 'NONE', #31972, #4780, #70812, .T. ) ;
#89406=ORIENTED_EDGE ( 'NONE', *, *, #19906, .T. ) ;
#89565=AXIS2_PLACEMENT_3D ( 'NONE', #57994, #50372, #28025 ) ;
#89572=PRODUCT_DEFINITION_SHAPE ( 'NONE', 'NONE',  #29568 ) ;
#89590=CARTESIAN_POINT ( 'NONE',  ( -8.160000000000000142, -10.65233964170348635, -1.621096496867198589 ) ) ;
#89596=ORIENTED_EDGE ( 'NONE', *, *, #12767, .F. ) ;
#89655=EDGE_CURVE ( 'NONE', #99448, #99058, #17830, .T. ) ;
#89663=DIRECTION ( 'NONE',  ( 0.000000000000000000, 0.000000000000000000, -1.000000000000000000 ) ) ;
#89674=DIRECTION ( 'NONE',  ( -1.000000000000000000, 0.000000000000000000, 0.000000000000000000 ) ) ;
#89738=EDGE_LOOP ( 'NONE', ( #30866, #26890, #55993 ) ) ;
#89779=CARTESIAN_POINT ( 'NONE',  ( 1.542438661763949392, 0.000000000000000000, 0.000000000000000000 ) ) ;
#89793=DIRECTION ( 'NONE',  ( 0.000000000000000000, 0.000000000000000000, -1.000000000000000000 ) ) ;
#89841=CIRCLE ( 'NONE', #46103, 1.699999999999999289 ) ;
#89863=ORIENTED_EDGE ( 'NONE', *, *, #21471, .F. ) ;
#89954=CARTESIAN_POINT ( 'NONE',  ( 8.160000000000000142, -6.754662360505033547, 7.925641719537454222 ) ) ;
#89957=DIRECTION ( 'NONE',  ( 0.000000000000000000, -0.9967269304714136968, -0.08084198211964954695 ) ) ;
#89995=CIRCLE ( 'NONE', #31759, 1.306876713926001354 ) ;
#90000=CARTESIAN_POINT ( 'NONE',  ( 7.160000000000000142, 0.1579206558577706254, 7.788828319098143105 ) ) ;
#90076=CARTESIAN_POINT ( 'NONE',  ( -6.660000000000001030, -5.396855673853237919E-16, 5.288828319098142217 ) ) ;
#90277=VECTOR ( 'NONE', #16001, 1000.000000000000000 ) ;
#90278=ORIENTED_EDGE ( 'NONE', *, *, #34135, .T. ) ;
#90294=DIRECTION ( 'NONE',  ( 0.000000000000000000, 0.000000000000000000, 1.000000000000000000 ) ) ;
#90390=EDGE_CURVE ( 'NONE', #21622, #74873, #21499, .T. ) ;
#90397=CARTESIAN_POINT ( 'NONE',  ( 1.542438661763949392, 0.000000000000000000, 0.000000000000000000 ) ) ;
#90537=ORIENTED_EDGE ( 'NONE', *, *, #93870, .F. ) ;
#90551=CARTESIAN_POINT ( 'NONE',  ( 7.160000000000000142, -6.754662360505033547, 7.925641719537454222 ) ) ;
#90623=CARTESIAN_POINT ( 'NONE',  ( 8.160000000000000142, -10.15233964170348457, 0.003711184059992174607 ) ) ;
#90647=ORIENTED_EDGE ( 'NONE', *, *, #86230, .F. ) ;
#90703=CARTESIAN_POINT ( 'NONE',  ( -8.160000000000000142, -10.65233964170348635, -1.621096496867198589 ) ) ;
#90772=DIRECTION ( 'NONE',  ( -1.000000000000000000, 0.000000000000000000, 0.000000000000000000 ) ) ;
#91041=DIRECTION ( 'NONE',  ( 0.000000000000000000, 0.000000000000000000, -1.000000000000000000 ) ) ;
#91055=DIRECTION ( 'NONE',  ( 1.000000000000000000, -0.000000000000000000, 0.000000000000000000 ) ) ;
#91088=DIRECTION ( 'NONE',  ( -1.000000000000000000, 0.000000000000000000, -0.000000000000000000 ) ) ;
#91133=CARTESIAN_POINT ( 'NONE',  ( -11.16000000000000014, -10.15233964170348457, 0.003711184059992174607 ) ) ;
#91149=EDGE_CURVE ( 'NONE', #26606, #82230, #28889, .T. ) ;
#91182=FACE_OUTER_BOUND ( 'NONE', #89738, .T. ) ;
#91259=DIRECTION ( 'NONE',  ( -1.000000000000000000, -0.000000000000000000, -0.000000000000000000 ) ) ;
#91310=DIRECTION ( 'NONE',  ( 1.000000000000000000, 0.000000000000000000, 0.000000000000000000 ) ) ;
#91377=ORIENTED_EDGE ( 'NONE', *, *, #91636, .T. ) ;
#91415=ORIENTED_EDGE ( 'NONE', *, *, #30525, .T. ) ;
#91534=ORIENTED_EDGE ( 'NONE', *, *, #55916, .F. ) ;
#91544=DIRECTION ( 'NONE',  ( 0.000000000000000000, 1.000000000000000000, 0.000000000000000000 ) ) ;
#91632=DIRECTION ( 'NONE',  ( 0.000000000000000000, 0.000000000000000000, -1.000000000000000000 ) ) ;
#91636=EDGE_CURVE ( 'NONE', #45450, #64237, #43614, .T. ) ;
#91644=LINE ( 'NONE', #58712, #65181 ) ;
#91651=ORIENTED_EDGE ( 'NONE', *, *, #9367, .T. ) ;
#91686=DIRECTION ( 'NONE',  ( 0.000000000000000000, -0.000000000000000000, -1.000000000000000000 ) ) ;
#91717=AXIS2_PLACEMENT_3D ( 'NONE', #49010, #80949, #79942 ) ;
#91948=FACE_OUTER_BOUND ( 'NONE', #84665, .T. ) ;
#91996=EDGE_LOOP ( 'NONE', ( #29478, #39464, #98609, #91534 ) ) ;
#92057=CARTESIAN_POINT ( 'NONE',  ( 8.160000000000000142, -2.890508098367099432, -0.2344417481469836528 ) ) ;
#92114=CARTESIAN_POINT ( 'NONE',  ( -7.426349086584751902, 10.80195425911416329, -0.9450485415980990345 ) ) ;
#92163=DIRECTION ( 'NONE',  ( 1.000000000000000000, 0.000000000000000000, 0.000000000000000000 ) ) ;
#92198=CARTESIAN_POINT ( 'NONE',  ( -8.160000000000000142, 0.1579206558577708475, 5.788828319098143105 ) ) ;
#92252=CARTESIAN_POINT ( 'NONE',  ( 6.660000000000001030, -9.123836073446797812, -2.666350264951732552 ) ) ;
#92293=AXIS2_PLACEMENT_3D ( 'NONE', #1559, #48743, #18275 ) ;
#92316=CARTESIAN_POINT ( 'NONE',  ( -8.160000000000000142, 1.682056942681651179, 5.192823660268256702 ) ) ;
#92330=CIRCLE ( 'NONE', #58828, 20.00000000000000000 ) ;
#92436=CARTESIAN_POINT ( 'NONE',  ( -8.160000000000000142, -5.907068460905240411E-16, 5.788828319098143105 ) ) ;
#92586=ORIENTED_EDGE ( 'NONE', *, *, #81428, .T. ) ;
#92589=ORIENTED_EDGE ( 'NONE', *, *, #34939, .F. ) ;
#92607=CARTESIAN_POINT ( 'NONE',  ( -8.134552738279960948, 10.05242149336743296, -0.8794729216540254635 ) ) ;
#92651=DIRECTION ( 'NONE',  ( 0.000000000000000000, 0.000000000000000000, -1.000000000000000000 ) ) ;
#92729=CYLINDRICAL_SURFACE ( 'NONE', #28974, 1.306876713926001798 ) ;
#92796=CARTESIAN_POINT ( 'NONE',  ( 8.160000000000000142, 0.1579206558577707364, 6.788828319098143105 ) ) ;
#92797=DIRECTION ( 'NONE',  ( -1.000000000000000000, 0.000000000000000000, 0.000000000000000000 ) ) ;
#92914=VERTEX_POINT ( 'NONE', #60681 ) ;
#92939=CARTESIAN_POINT ( 'NONE',  ( -7.160000000000000142, 1.682056942681651401, 5.192823660268256702 ) ) ;
#92956=EDGE_CURVE ( 'NONE', #41964, #26321, #48551, .T. ) ;
#93106=ADVANCED_FACE ( 'NONE', ( #82373 ), #75256, .T. ) ;
#93168=CARTESIAN_POINT ( 'NONE',  ( 6.660000000000001030, -9.074990544709798712, -0.7360493640965781736 ) ) ;
#93317=VECTOR ( 'NONE', #18215, 1000.000000000000000 ) ;
#93370=EDGE_LOOP ( 'NONE', ( #82412, #87368, #36969, #41694, #54758, #14942, #77682, #17988, #52427, #10017 ) ) ;
#93384=DIRECTION ( 'NONE',  ( -1.000000000000000000, 0.000000000000000000, 0.000000000000000000 ) ) ;
#93434=VECTOR ( 'NONE', #77923, 1000.000000000000114 ) ;
#93439=LINE ( 'NONE', #39161, #46455 ) ;
#93460=ORIENTED_EDGE ( 'NONE', *, *, #31358, .F. ) ;
#93473=ORIENTED_EDGE ( 'NONE', *, *, #22218, .F. ) ;
#93493=EDGE_LOOP ( 'NONE', ( #29363, #78077, #6313, #48944, #82006, #65813 ) ) ;
#93514=AXIS2_PLACEMENT_3D ( 'NONE', #86975, #80873, #72772 ) ;
#93605=CARTESIAN_POINT ( 'NONE',  ( 7.160000000000000142, 8.500000000000000000, 6.788828319098143993 ) ) ;
#93631=EDGE_CURVE ( 'NONE', #18728, #71622, #54930, .T. ) ;
#93789=DIRECTION ( 'NONE',  ( 0.000000000000000000, 0.000000000000000000, -1.000000000000000000 ) ) ;
#93794=DIRECTION ( 'NONE',  ( -1.000000000000000000, 0.000000000000000000, 0.000000000000000000 ) ) ;
#93848=ORIENTED_EDGE ( 'NONE', *, *, #16327, .T. ) ;
#93870=EDGE_CURVE ( 'NONE', #21622, #72523, #83250, .T. ) ;
#93929=ORIENTED_EDGE ( 'NONE', *, *, #89394, .T. ) ;
#93948=CYLINDRICAL_SURFACE ( 'NONE', #39933, 1.000000000000000222 ) ;
#93973=VERTEX_POINT ( 'NONE', #47706 ) ;
#93983=CARTESIAN_POINT ( 'NONE',  ( -6.660000000000001030, 0.000000000000000000, 0.000000000000000000 ) ) ;
#94081=VECTOR ( 'NONE', #7408, 1000.000000000000000 ) ;
#94093=ORIENTED_EDGE ( 'NONE', *, *, #6485, .T. ) ;
#94172=DIRECTION ( 'NONE',  ( 0.000000000000000000, 0.000000000000000000, 1.000000000000000000 ) ) ;
#94182=DIRECTION ( 'NONE',  ( 1.000000000000000000, -0.000000000000000000, -0.000000000000000000 ) ) ;
#94248=DIRECTION ( 'NONE',  ( -1.000000000000000000, 0.000000000000000000, 0.000000000000000000 ) ) ;
#94334=PLANE ( 'NONE',  #85129 ) ;
#94354=TOROIDAL_SURFACE ( 'NONE', #23058, 19.00000000000000000, 1.000000000000000000 ) ;
#94363=EDGE_LOOP ( 'NONE', ( #76767, #53317, #47611, #60177, #58023, #2306 ) ) ;
#94420=ORIENTED_EDGE ( 'NONE', *, *, #93631, .T. ) ;
#94564=ADVANCED_FACE ( 'NONE', ( #91182 ), #8452, .T. ) ;
#94676=FACE_OUTER_BOUND ( 'NONE', #77857, .T. ) ;
#94908=DIRECTION ( 'NONE',  ( 0.000000000000000000, 0.000000000000000000, -1.000000000000000000 ) ) ;
#94929=FACE_OUTER_BOUND ( 'NONE', #74808, .T. ) ;
#94951=EDGE_CURVE ( 'NONE', #82135, #57944, #66765, .T. ) ;
#95031=DIRECTION ( 'NONE',  ( 0.000000000000000000, 0.000000000000000000, -1.000000000000000000 ) ) ;
#95068=VERTEX_POINT ( 'NONE', #53524 ) ;
#95086=AXIS2_PLACEMENT_3D ( 'NONE', #72172, #2663, #66076 ) ;
#95099=ORIENTED_EDGE ( 'NONE', *, *, #54719, .T. ) ;
#95106=ORIENTED_EDGE ( 'NONE', *, *, #32029, .F. ) ;
#95126=ORIENTED_EDGE ( 'NONE', *, *, #16359, .T. ) ;
#95143=ORIENTED_EDGE ( 'NONE', *, *, #51643, .T. ) ;
#95146=ORIENTED_EDGE ( 'NONE', *, *, #41073, .F. ) ;
#95161=ORIENTED_EDGE ( 'NONE', *, *, #41567, .T. ) ;
#95187=CARTESIAN_POINT ( 'NONE',  ( 8.160000000000000142, -10.15233964170348457, 1.310587897985993955 ) ) ;
#95305=DIRECTION ( 'NONE',  ( 0.000000000000000000, -1.000000000000000000, -1.020425574104004246E-16 ) ) ;
#95325=CARTESIAN_POINT ( 'NONE',  ( -8.160000000000000142, -10.15233964170348457, 0.003711184059992174607 ) ) ;
#95337=CARTESIAN_POINT ( 'NONE',  ( -7.160000000000000142, -6.754662360505033547, 7.925641719537454222 ) ) ;
#95370=ORIENTED_EDGE ( 'NONE', *, *, #47716, .T. ) ;
#95442=CYLINDRICAL_SURFACE ( 'NONE', #28277, 18.50000000000000355 ) ;
#95594=DIRECTION ( 'NONE',  ( 1.000000000000000000, -0.000000000000000000, 0.000000000000000000 ) ) ;
#95637=PLANE ( 'NONE',  #20689 ) ;
#95839=DIRECTION ( 'NONE',  ( 0.000000000000000000, 0.000000000000000000, -1.000000000000000000 ) ) ;
#95865=CARTESIAN_POINT ( 'NONE',  ( 8.160000000000000142, -9.652339641703484574, -1.621096496867199033 ) ) ;
#95866=ORIENTED_EDGE ( 'NONE', *, *, #2022, .F. ) ;
#95950=VECTOR ( 'NONE', #95305, 1000.000000000000000 ) ;
#95957=DIRECTION ( 'NONE',  ( 0.000000000000000000, 0.000000000000000000, -1.000000000000000000 ) ) ;
#96063=FACE_OUTER_BOUND ( 'NONE', #79600, .T. ) ;
#96074=FACE_OUTER_BOUND ( 'NONE', #42480, .T. ) ;
#96119=DIRECTION ( 'NONE',  ( 0.000000000000000000, 0.000000000000000000, -1.000000000000000000 ) ) ;
#96124=CARTESIAN_POINT ( 'NONE',  ( -6.660000000000001030, -9.074990544709798712, -0.7360493640965779516 ) ) ;
#96139=ORIENTED_EDGE ( 'NONE', *, *, #28139, .F. ) ;
#96310=AXIS2_PLACEMENT_3D ( 'NONE', #45188, #7111, #69013 ) ;
#96329=EDGE_CURVE ( 'NONE', #39981, #61060, #20933, .T. ) ;
#96493=CARTESIAN_POINT ( 'NONE',  ( 6.660000000000001030, 7.578413286920094194, 5.288828319098143105 ) ) ;
#96499=AXIS2_PLACEMENT_3D ( 'NONE', #68729, #37774, #76317 ) ;
#96588=CARTESIAN_POINT ( 'NONE',  ( 8.160000000000000142, -10.15233964170348457, 0.003711184059992174607 ) ) ;
#96598=DIRECTION ( 'NONE',  ( 0.000000000000000000, 0.000000000000000000, -1.000000000000000000 ) ) ;
#96603=CARTESIAN_POINT ( 'NONE',  ( 8.160000000000000142, 1.020006686409831046E-16, 5.788828319098143105 ) ) ;
#96605=LINE ( 'NONE', #48451, #15869 ) ;
#96632=ORIENTED_EDGE ( 'NONE', *, *, #27449, .T. ) ;
#96713=CIRCLE ( 'NONE', #52981, 1.306876713926001354 ) ;
#96753=ORIENTED_EDGE ( 'NONE', *, *, #20331, .T. ) ;
#96768=CIRCLE ( 'NONE', #53029, 1.699999999999999289 ) ;
#96798=DIRECTION ( 'NONE',  ( -0.000000000000000000, 0.9513357669802769978, -0.3081562241202472907 ) ) ;
#96866=VECTOR ( 'NONE', #29464, 1000.000000000000000 ) ;
#96991=LINE ( 'NONE', #27490, #96866 ) ;
#97010=AXIS2_PLACEMENT_3D ( 'NONE', #14448, #74851, #81980 ) ;
#97032=AXIS2_PLACEMENT_3D ( 'NONE', #78943, #32279, #8444 ) ;
#97057=LINE ( 'NONE', #26558, #21396 ) ;
#97100=LINE ( 'NONE', #80880, #51114 ) ;
#97138=ORIENTED_EDGE ( 'NONE', *, *, #86156, .T. ) ;
#97175=DIRECTION ( 'NONE',  ( -1.000000000000000000, 0.000000000000000000, -0.000000000000000000 ) ) ;
#97281=ORIENTED_EDGE ( 'NONE', *, *, #62519, .T. ) ;
#97291=CARTESIAN_POINT ( 'NONE',  ( 6.660000000000001030, 2.939152317953647106E-16, -2.399999999999999911 ) ) ;
#97296=AXIS2_PLACEMENT_3D ( 'NONE', #41642, #40129, #1068 ) ;
#97302=LINE ( 'NONE', #4952, #4948 ) ;
#97313=DIRECTION ( 'NONE',  ( -1.000000000000000000, 0.000000000000000000, -0.000000000000000000 ) ) ;
#97396=DIRECTION ( 'NONE',  ( 0.000000000000000000, 0.000000000000000000, 1.000000000000000000 ) ) ;
#97408=AXIS2_PLACEMENT_3D ( 'NONE', #74812, #45387, #91041 ) ;
#97508=DIRECTION ( 'NONE',  ( 0.000000000000000000, 0.000000000000000000, 1.000000000000000000 ) ) ;
#97524=AXIS2_PLACEMENT_3D ( 'NONE', #13508, #27753, #20133 ) ;
#97538=EDGE_CURVE ( 'NONE', #27461, #48074, #43765, .T. ) ;
#97568=LINE ( 'NONE', #67144, #58056 ) ;
#97595=VERTEX_POINT ( 'NONE', #42167 ) ;
#97633=VERTEX_POINT ( 'NONE', #52394 ) ;
#97647=EDGE_CURVE ( 'NONE', #65066, #87928, #22414, .T. ) ;
#97935=VECTOR ( 'NONE', #62898, 1000.000000000000000 ) ;
#97944=DIRECTION ( 'NONE',  ( 1.000000000000000000, -0.000000000000000000, -0.000000000000000000 ) ) ;
#98075=CARTESIAN_POINT ( 'NONE',  ( -6.660000000000001030, 0.000000000000000000, 2.399999999999999911 ) ) ;
#98092=DIRECTION ( 'NONE',  ( 0.000000000000000000, 0.000000000000000000, -1.000000000000000000 ) ) ;
#98138=CARTESIAN_POINT ( 'NONE',  ( 7.160000000000000142, 10.80195425911416507, -0.9450485415980990345 ) ) ;
#98223=CARTESIAN_POINT ( 'NONE',  ( -7.962149653358833845, 10.40864506560536462, -0.9106384459055537617 ) ) ;
#98249=DIRECTION ( 'NONE',  ( -1.000000000000000000, -0.000000000000000000, -0.000000000000000000 ) ) ;
#98261=CARTESIAN_POINT ( 'NONE',  ( -6.660000000000001030, 9.283009703645923594, -0.8121581124701985344 ) ) ;
#98264=CARTESIAN_POINT ( 'NONE',  ( -8.160000000000000142, -10.15233964170348457, 0.003711184059992174607 ) ) ;
#98300=CIRCLE ( 'NONE', #36756, 1.000000000000000222 ) ;
#98304=DIRECTION ( 'NONE',  ( 0.000000000000000000, 0.000000000000000000, -1.000000000000000000 ) ) ;
#98495=ORIENTED_EDGE ( 'NONE', *, *, #97647, .T. ) ;
#98518=DIRECTION ( 'NONE',  ( 0.000000000000000000, 2.688821387764050602E-15, -1.000000000000000000 ) ) ;
#98537=EDGE_CURVE ( 'NONE', #46703, #56978, #1686, .T. ) ;
#98598=EDGE_CURVE ( 'NONE', #82135, #42245, #25943, .T. ) ;
#98609=ORIENTED_EDGE ( 'NONE', *, *, #69460, .T. ) ;
#98627=VERTEX_POINT ( 'NONE', #61164 ) ;
#98648=ORIENTED_EDGE ( 'NONE', *, *, #10014, .T. ) ;
#98752=CARTESIAN_POINT ( 'NONE',  ( 8.160000000000000142, 8.793627758918228565, -2.994553991265763049 ) ) ;
#98831=ORIENTED_EDGE ( 'NONE', *, *, #69011, .F. ) ;
#98905=CARTESIAN_POINT ( 'NONE',  ( -6.660000000000001030, -10.15233964170348457, 0.003711184059992174607 ) ) ;
#98967=EDGE_LOOP ( 'NONE', ( #23332, #22069, #58953, #48875 ) ) ;
#99029=DIRECTION ( 'NONE',  ( 0.000000000000000000, -0.000000000000000000, -1.000000000000000000 ) ) ;
#99058=VERTEX_POINT ( 'NONE', #22433 ) ;
#99147=VERTEX_POINT ( 'NONE', #41072 ) ;
#99155=EDGE_CURVE ( 'NONE', #45368, #26606, #34954, .T. ) ;
#99230=VECTOR ( 'NONE', #22263, 1000.000000000000000 ) ;
#99262=EDGE_CURVE ( 'NONE', #61766, #39981, #60802, .T. ) ;
#99275=PLANE ( 'NONE',  #69101 ) ;
#99344=ORIENTED_EDGE ( 'NONE', *, *, #82517, .T. ) ;
#99389=FACE_OUTER_BOUND ( 'NONE', #59616, .T. ) ;
#99440=AXIS2_PLACEMENT_3D ( 'NONE', #35413, #96798, #11553 ) ;
#99448=VERTEX_POINT ( 'NONE', #17612 ) ;
#99516=DIRECTION ( 'NONE',  ( 1.000000000000000000, -0.000000000000000000, 0.000000000000000000 ) ) ;
#99557=VECTOR ( 'NONE', #76442, 1000.000000000000000 ) ;
#99674=CIRCLE ( 'NONE', #52704, 1.000000000000000000 ) ;
#99694=EDGE_LOOP ( 'NONE', ( #95106, #64935, #64611, #30360 ) ) ;
#99706=CARTESIAN_POINT ( 'NONE',  ( -8.035485827249791768, 10.29661271514167709, -0.9008368852918171577 ) ) ;
#99708=CARTESIAN_POINT ( 'NONE',  ( -8.160000000000000142, 7.891155995661686795, 5.788828319098143993 ) ) ;
#99710=AXIS2_PLACEMENT_3D ( 'NONE', #58643, #43428, #9592 ) ;
#99722=CARTESIAN_POINT ( 'NONE',  ( 6.660000000000001030, 0.000000000000000000, 0.000000000000000000 ) ) ;
#99731=CARTESIAN_POINT ( 'NONE',  ( -11.16000000000000014, -10.15233964170348457, 0.003711184059992174607 ) ) ;
#99820=CARTESIAN_POINT ( 'NONE',  ( 7.160000000000000142, 3.920813812768718080E-16, 6.788828319098143105 ) ) ;
#99840=EDGE_CURVE ( 'NONE', #57944, #86101, #27605, .T. ) ;
#99968=ORIENTED_EDGE ( 'NONE', *, *, #89655, .F. ) ;
#100030=ORIENTED_EDGE ( 'NONE', *, *, #34236, .F. ) ;
#100051=CARTESIAN_POINT ( 'NONE',  ( 7.160000000000000142, 7.891155995661686795, 5.788828319098143993 ) ) ;
#100084=AXIS2_PLACEMENT_3D ( 'NONE', #60448, #82262, #36582 ) ;
#100103=CIRCLE ( 'NONE', #77447, 2.399999999999999911 ) ;
#100129=PLANE ( 'NONE',  #55739 ) ;
#100187=ORIENTED_EDGE ( 'NONE', *, *, #81963, .T. ) ;
#100200=DIRECTION ( 'NONE',  ( 1.000000000000000000, -0.000000000000000000, 0.000000000000000000 ) ) ;
#100384=CARTESIAN_POINT ( 'NONE',  ( 16.36243866176394945, 2.939152317953647106E-16, -2.399999999999999911 ) ) ;
#100441=COLOUR_RGB('Light Blue', 0.31764706, 0.68627451, 0.89019608);
#100442=FILL_AREA_STYLE_COLOUR('',#100441);
#100443=FILL_AREA_STYLE('',(#100442));
#100444=SURFACE_STYLE_FILL_AREA(#100443);
#100445=SURFACE_SIDE_STYLE('',(#100444));
#100446=SURFACE_STYLE_USAGE(.BOTH.,#100445);
#100447=PRESENTATION_STYLE_ASSIGNMENT((#100446));
#100488=STYLED_ITEM('',(#100447),#8332);
#100489=MECHANICAL_DESIGN_GEOMETRIC_PRESENTATION_REPRESENTATION('',(#100488),#48843);
ENDSEC;
END-ISO-10303-21;
